ISO-10303-21;
HEADER;
FILE_DESCRIPTION (('STEP AP214'),
    '1' );
FILE_NAME ('hex flange nut gradea_iso_ISO - 4161 - M5 - N.step',
    '2026-10-08T11:45:07',
    ( '' ),
    ( '' ),
    'SwSTEP 2.0',
    'SolidWorks 2026',
    '' );
FILE_SCHEMA (( 'AUTOMOTIVE_DESIGN' ));
ENDSEC;

DATA;
#59=EDGE_LOOP ( 'NONE', ( #27677, #9320, #7424, #19818 ) ) ;
#73=CONICAL_SURFACE ( 'NONE', #24545, 4.000000000000000000, 0.8911886515913786111 ) ;
#84=ORIENTED_EDGE ( 'NONE', *, *, #2078, .T. ) ;
#92=CIRCLE ( 'NONE', #23863, 2.500000000000000888 ) ;
#95=B_SPLINE_CURVE_WITH_KNOTS ( 'NONE', 3,
 ( #42025, #12179, #25497, #38758, #5606, #41162, #34637, #4752 ),
 .UNSPECIFIED., .F., .F.,
 ( 4, 2, 2, 4 ),
 ( 2.465131517071352357E-07, 0.001183067374689843057, 0.001774477805458910071, 0.002365888236227977302 ),
 .UNSPECIFIED. ) ;
#128=DIRECTION ( 'NONE',  ( -0.8660254037844377084, -0.5000000000000015543, 0.000000000000000000 ) ) ;
#140=CARTESIAN_POINT ( 'NONE',  ( -2.688821387764050996E-14, -4.618802153517012954, -0.4999999999999995559 ) ) ;
#195=ORIENTED_EDGE ( 'NONE', *, *, #39418, .T. ) ;
#211=( LENGTH_UNIT ( ) NAMED_UNIT ( * ) SI_UNIT ( .MILLI., .METRE. ) );
#261=ORIENTED_EDGE ( 'NONE', *, *, #7947, .F. ) ;
#271=CARTESIAN_POINT ( 'NONE',  ( 3.453038570460273071, 2.625189405340834448, -3.535263753543585352 ) ) ;
#297=CARTESIAN_POINT ( 'NONE',  ( 4.197478902586992966, -0.8524102783748346290, -3.505063281295504041 ) ) ;
#371=CARTESIAN_POINT ( 'NONE',  ( -4.000000000000000000, -2.309401076758512694, -5.000000000000000000 ) ) ;
#414=DIRECTION ( 'NONE',  ( 0.000000000000000000, 0.000000000000000000, -1.000000000000000000 ) ) ;
#460=FACE_OUTER_BOUND ( 'NONE', #18537, .T. ) ;
#512=CARTESIAN_POINT ( 'NONE',  ( -0.1756481739660520902, 4.720212674038980261, -3.469390959564065291 ) ) ;
#518=ORIENTED_EDGE ( 'NONE', *, *, #39998, .F. ) ;
#539=DIRECTION ( 'NONE',  ( 0.000000000000000000, 0.000000000000000000, -1.000000000000000000 ) ) ;
#584=ORIENTED_EDGE ( 'NONE', *, *, #31908, .F. ) ;
#613=CARTESIAN_POINT ( 'NONE',  ( 0.000000000000000000, 0.000000000000000000, 0.000000000000000000 ) ) ;
#622=B_SPLINE_CURVE_WITH_KNOTS ( 'NONE', 3,
 ( #39665, #43157, #13743, #26398, #40087 ),
 .UNSPECIFIED., .F., .F.,
 ( 4, 1, 4 ),
 ( 0.000000000000000000, 0.002309401076758505790, 0.004618802153517011580 ),
 .UNSPECIFIED. ) ;
#651=ADVANCED_FACE ( 'NONE', ( #42509 ), #30274, .T. ) ;
#744=CARTESIAN_POINT ( 'NONE',  ( 4.204115023516791005, -1.660442669500199919, -3.602151381774560068 ) ) ;
#754=UNCERTAINTY_MEASURE_WITH_UNIT (LENGTH_MEASURE( 1.000000000000000082E-05 ), #18890, 'distance_accuracy_value', 'NONE');
#880=VERTEX_POINT ( 'NONE', #27042 ) ;
#886=DIRECTION ( 'NONE',  ( -1.000000000000000000, 0.000000000000000000, 0.000000000000000000 ) ) ;
#921=( GEOMETRIC_REPRESENTATION_CONTEXT ( 3 ) GLOBAL_UNCERTAINTY_ASSIGNED_CONTEXT ( ( #23939 ) ) GLOBAL_UNIT_ASSIGNED_CONTEXT ( ( #36668, #19284, #23199 ) ) REPRESENTATION_CONTEXT ( 'NONE', 'WORKASPACE' ) );
#925=CARTESIAN_POINT ( 'NONE',  ( -4.000000000000000000, -2.309401076758512694, -3.433295621305382461 ) ) ;
#946=ORIENTED_EDGE ( 'NONE', *, *, #39507, .T. ) ;
#959=VERTEX_POINT ( 'NONE', #25095 ) ;
#960=FACE_OUTER_BOUND ( 'NONE', #43029, .T. ) ;
#971=CARTESIAN_POINT ( 'NONE',  ( -2.059999999999998721, 2.522772406243545965E-16, -0.3080913168122742518 ) ) ;
#973=FACE_OUTER_BOUND ( 'NONE', #23662, .T. ) ;
#984=ORIENTED_EDGE ( 'NONE', *, *, #40319, .F. ) ;
#985=ADVANCED_FACE ( 'NONE', ( #21393 ), #5177, .F. ) ;
#989=CARTESIAN_POINT ( 'NONE',  ( 2.000000000000008882, 3.464101615137749945, 0.000000000000000000 ) ) ;
#992=ORIENTED_EDGE ( 'NONE', *, *, #4759, .F. ) ;
#1044=EDGE_CURVE ( 'NONE', #28956, #25474, #28562, .T. ) ;
#1069=DIRECTION ( 'NONE',  ( 0.000000000000000000, 0.000000000000000000, -1.000000000000000000 ) ) ;
#1070=CARTESIAN_POINT ( 'NONE',  ( -4.000000000000000000, -1.560351142792950618, -0.2242961665059814425 ) ) ;
#1085=DIRECTION ( 'NONE',  ( 0.5000000000000022204, 0.8660254037844374864, -0.000000000000000000 ) ) ;
#1123=VECTOR ( 'NONE', #42915, 1000.000000000000000 ) ;
#1167=CYLINDRICAL_SURFACE ( 'NONE', #25601, 2.500000000000000444 ) ;
#1169=AXIS2_PLACEMENT_3D ( 'NONE', #25224, #31311, #41088 ) ;
#1184=EDGE_CURVE ( 'NONE', #19145, #1657, #25354, .T. ) ;
#1211=VECTOR ( 'NONE', #11533, 1000.000000000000000 ) ;
#1218=EDGE_CURVE ( 'NONE', #29305, #30609, #4032, .T. ) ;
#1241=CARTESIAN_POINT ( 'NONE',  ( 2.290893957444128645E-15, 4.647089433458768681, -3.572167766733382877 ) ) ;
#1255=EDGE_LOOP ( 'NONE', ( #36454, #18678, #2896, #13801 ) ) ;
#1265=CARTESIAN_POINT ( 'NONE',  ( -0.1404048886732797152, -4.699864953788083888, -3.686887068327043160 ) ) ;
#1290=CARTESIAN_POINT ( 'NONE',  ( -2.100000000000000089, 2.571758278209441957E-16, -4.694516984716113228 ) ) ;
#1342=CARTESIAN_POINT ( 'NONE',  ( -1.257172072275743346, 3.892973519171203378, -3.433252694550776862 ) ) ;
#1357=CARTESIAN_POINT ( 'NONE',  ( -4.000000000000000000, 2.471528634177585282, -3.686887442155186712 ) ) ;
#1474=ORIENTED_EDGE ( 'NONE', *, *, #10997, .F. ) ;
#1518=EDGE_LOOP ( 'NONE', ( #6252, #2651, #27456, #24851 ) ) ;
#1521=CARTESIAN_POINT ( 'NONE',  ( 0.000000000000000000, 0.000000000000000000, 0.000000000000000000 ) ) ;
#1535=ORIENTED_EDGE ( 'NONE', *, *, #4676, .T. ) ;
#1572=CARTESIAN_POINT ( 'NONE',  ( -4.000000000000000000, 0.8576368993457507139, -3.433240632782198709 ) ) ;
#1611=DIRECTION ( 'NONE',  ( -0.000000000000000000, -0.000000000000000000, 1.000000000000000000 ) ) ;
#1657=VERTEX_POINT ( 'NONE', #2471 ) ;
#1741=B_SPLINE_CURVE_WITH_KNOTS ( 'NONE', 3,
 ( #35894, #5599, #29597, #12170, #36120, #28962 ),
 .UNSPECIFIED., .F., .F.,
 ( 4, 2, 4 ),
 ( 0.000000000000000000, 0.0002095117440854740156, 0.0004190234881709480313 ),
 .UNSPECIFIED. ) ;
#1758=CONICAL_SURFACE ( 'NONE', #26878, 4.000000000000000000, 0.8911886515913786111 ) ;
#1776=ORIENTED_EDGE ( 'NONE', *, *, #7769, .F. ) ;
#1848=CARTESIAN_POINT ( 'NONE',  ( -4.000000000000000000, 0.3987449864459974846, -0.01220643443059782861 ) ) ;
#1858=VERTEX_POINT ( 'NONE', #20857 ) ;
#1914=ORIENTED_EDGE ( 'NONE', *, *, #17311, .T. ) ;
#1934=CARTESIAN_POINT ( 'NONE',  ( 1.317756351988342622, -3.857995168970215438, -0.04852650426602527628 ) ) ;
#1960=EDGE_CURVE ( 'NONE', #25462, #7155, #40191, .T. ) ;
#2000=CARTESIAN_POINT ( 'NONE',  ( 0.000000000000000000, 0.000000000000000000, -4.974599999999998801 ) ) ;
#2015=LINE ( 'NONE', #28029, #1123 ) ;
#2022=ORIENTED_EDGE ( 'NONE', *, *, #26835, .F. ) ;
#2078=EDGE_CURVE ( 'NONE', #9725, #29305, #22099, .T. ) ;
#2123=CARTESIAN_POINT ( 'NONE',  ( 4.000000000000000000, -1.560351142792952617, -0.2242961665059816367 ) ) ;
#2125=ORIENTED_EDGE ( 'NONE', *, *, #9438, .F. ) ;
#2248=ORIENTED_EDGE ( 'NONE', *, *, #42790, .F. ) ;
#2299=ORIENTED_EDGE ( 'NONE', *, *, #39507, .F. ) ;
#2307=ADVANCED_FACE ( 'NONE', ( #8466, #22254 ), #2316, .F. ) ;
#2316=PLANE ( 'NONE',  #3104 ) ;
#2471=CARTESIAN_POINT ( 'NONE',  ( 1.411581201560190495E-15, 4.862606272033091592, -3.745885042887436622 ) ) ;
#2560=EDGE_CURVE ( 'NONE', #6569, #3149, #21658, .T. ) ;
#2588=AXIS2_PLACEMENT_3D ( 'NONE', #33198, #16207, #6791 ) ;
#2651=ORIENTED_EDGE ( 'NONE', *, *, #27048, .T. ) ;
#2681=PLANE ( 'NONE',  #26554 ) ;
#2737=CARTESIAN_POINT ( 'NONE',  ( 4.000000000000000000, -2.309401076758514915, -3.433295621305383349 ) ) ;
#2739=CARTESIAN_POINT ( 'NONE',  ( -0.3198814748697807464, -4.434118497892185040, -0.3507732604232532969 ) ) ;
#2787=ORIENTED_EDGE ( 'NONE', *, *, #5774, .F. ) ;
#2824=CARTESIAN_POINT ( 'NONE',  ( -6.473970235329672780E-16, -4.862606272033106691, -3.745885042887442395 ) ) ;
#2896=ORIENTED_EDGE ( 'NONE', *, *, #26699, .F. ) ;
#2924=CARTESIAN_POINT ( 'NONE',  ( -6.259644161404860030E-16, -4.618802153517027165, -3.433295621305388234 ) ) ;
#2936=ORIENTED_EDGE ( 'NONE', *, *, #29273, .T. ) ;
#2939=DIRECTION ( 'NONE',  ( 0.000000000000000000, 0.000000000000000000, 1.000000000000000000 ) ) ;
#2970=CARTESIAN_POINT ( 'NONE',  ( 4.154306624731137099, 2.398490048084935822, -3.721999068284414847 ) ) ;
#3104=AXIS2_PLACEMENT_3D ( 'NONE', #18981, #25101, #21827 ) ;
#3149=VERTEX_POINT ( 'NONE', #925 ) ;
#3197=CARTESIAN_POINT ( 'NONE',  ( 3.680118525130245732, -2.494084732383344605, -0.3507732604232533524 ) ) ;
#3232=DIRECTION ( 'NONE',  ( -1.000000000000000000, 0.000000000000000000, 0.000000000000000000 ) ) ;
#3251=DIRECTION ( 'NONE',  ( -0.000000000000000000, 0.000000000000000000, -1.000000000000000000 ) ) ;
#3265=B_SPLINE_CURVE_WITH_KNOTS ( 'NONE', 3,
 ( #18482, #14547, #1848, #17829, #31536, #31104, #34801, #15210 ),
 .UNSPECIFIED., .F., .F.,
 ( 4, 2, 2, 4 ),
 ( 0.005725059856848641743, 0.006314084072593626612, 0.006903108288338611481, 0.008081156719828581220 ),
 .UNSPECIFIED. ) ;
#3275=AXIS2_PLACEMENT_3D ( 'NONE', #14499, #27811, #4643 ) ;
#3470=CARTESIAN_POINT ( 'NONE',  ( 0.000000000000000000, 0.000000000000000000, 0.000000000000000000 ) ) ;
#3496=FILL_AREA_STYLE ('',( #23408 ) ) ;
#3518=CARTESIAN_POINT ( 'NONE',  ( 2.000000000000008882, 3.464101615137749945, 0.000000000000000000 ) ) ;
#3553=CARTESIAN_POINT ( 'NONE',  ( 3.540020015735602765, 2.810662092924382627, -3.602146406945867962 ) ) ;
#3559=APPLICATION_CONTEXT ( 'automotive_design' ) ;
#3563=DIRECTION ( 'NONE',  ( -0.000000000000000000, -0.000000000000000000, 1.000000000000000000 ) ) ;
#3653=EDGE_LOOP ( 'NONE', ( #27977, #6731, #35715, #37933 ) ) ;
#3674=CARTESIAN_POINT ( 'NONE',  ( 4.000000000000000000, 0.1981133338132474442, 2.382280164152719704E-17 ) ) ;
#3736=ORIENTED_EDGE ( 'NONE', *, *, #30113, .T. ) ;
#3802=DIRECTION ( 'NONE',  ( -0.8191520442889875797, 1.003171929053519570E-16, 0.5735764363510522656 ) ) ;
#3852=CARTESIAN_POINT ( 'NONE',  ( 0.000000000000000000, 0.000000000000000000, 0.000000000000000000 ) ) ;
#3862=COLOUR_RGB ( '', 0.31764706, 0.68627451, 0.89019608) ;
#3894=CARTESIAN_POINT ( 'NONE',  ( -2.804994570502171047, -3.229033611042465335, -3.526374918436838701 ) ) ;
#3982=CARTESIAN_POINT ( 'NONE',  ( 1.567478505476134606E-15, 4.618802153517012066, -5.000000000000000000 ) ) ;
#4019=CARTESIAN_POINT ( 'NONE',  ( 4.000000000000000000, -1.700175430507292473, -3.320327275037661785 ) ) ;
#4032=LINE ( 'NONE', #971, #36056 ) ;
#4036=VERTEX_POINT ( 'NONE', #42313 ) ;
#4069=DIRECTION ( 'NONE',  ( 1.000000000000000000, 0.000000000000000000, 0.000000000000000000 ) ) ;
#4142=FACE_OUTER_BOUND ( 'NONE', #25674, .T. ) ;
#4190=ADVANCED_FACE ( 'NONE', ( #19858 ), #30733, .T. ) ;
#4219=DIRECTION ( 'NONE',  ( 1.000000000000000000, 0.000000000000000000, 0.000000000000000000 ) ) ;
#4280=FACE_OUTER_BOUND ( 'NONE', #13855, .T. ) ;
#4316=DIRECTION ( 'NONE',  ( -0.000000000000000000, 0.000000000000000000, -1.000000000000000000 ) ) ;
#4406=CARTESIAN_POINT ( 'NONE',  ( 4.211140560182196957, -2.431303136016555122, -3.745885042887436622 ) ) ;
#4466=DIRECTION ( 'NONE',  ( -1.000000000000000000, 0.000000000000000000, 0.000000000000000000 ) ) ;
#4566=ADVANCED_FACE ( 'NONE', ( #25098 ), #24891, .F. ) ;
#4615=CARTESIAN_POINT ( 'NONE',  ( 0.02448733951239481094, 4.877042772274728044, -3.751161874094022242 ) ) ;
#4635=DIRECTION ( 'NONE',  ( -1.000000000000000000, 1.224646799147352714E-16, 0.000000000000000000 ) ) ;
#4643=DIRECTION ( 'NONE',  ( -1.000000000000000000, 0.000000000000000000, 0.000000000000000000 ) ) ;
#4666=CIRCLE ( 'NONE', #1169, 4.000000000000000000 ) ;
#4668=AXIS2_PLACEMENT_3D ( 'NONE', #40585, #22998, #36241 ) ;
#4676=EDGE_CURVE ( 'NONE', #24669, #20680, #4931, .T. ) ;
#4730=AXIS2_PLACEMENT_3D ( 'NONE', #15806, #15183, #22166 ) ;
#4752=CARTESIAN_POINT ( 'NONE',  ( -2.000000000000006661, 3.464101615137750834, 0.000000000000000000 ) ) ;
#4759=EDGE_CURVE ( 'NONE', #20305, #7155, #40647, .T. ) ;
#4817=CONICAL_SURFACE ( 'NONE', #31987, 2.059999999999998721, 0.9599310885968738161 ) ;
#4842=CARTESIAN_POINT ( 'NONE',  ( -3.522875095019672109, 2.820352903225427532, -3.598441714920591394 ) ) ;
#4856=CARTESIAN_POINT ( 'NONE',  ( -4.000000000000000000, 1.677772373332757194, -3.535253723897187506 ) ) ;
#4894=CARTESIAN_POINT ( 'NONE',  ( -2.100000000000000089, 2.571758278209441957E-16, -0.2800830152838844622 ) ) ;
#4895=EDGE_CURVE ( 'NONE', #24356, #40010, #33478, .T. ) ;
#4912=DIRECTION ( 'NONE',  ( -0.000000000000000000, -0.000000000000000000, 1.000000000000000000 ) ) ;
#4931=CIRCLE ( 'NONE', #11903, 2.500000000000000444 ) ;
#4954=CARTESIAN_POINT ( 'NONE',  ( 1.567478505476135000E-15, 4.618802153517012954, -3.504269196027527844 ) ) ;
#4976=CARTESIAN_POINT ( 'NONE',  ( 1.243802165048773611, -3.900692638707475624, -3.223146290109810241 ) ) ;
#5059=CARTESIAN_POINT ( 'NONE',  ( 1.393927851585479161, -4.043713361053543842, -3.526374918436840922 ) ) ;
#5070=CARTESIAN_POINT ( 'NONE',  ( 4.197393957002303999, -0.4069871074557456780, -3.503767560748925813 ) ) ;
#5130=ORIENTED_EDGE ( 'NONE', *, *, #16089, .T. ) ;
#5177=CYLINDRICAL_SURFACE ( 'NONE', #15225, 2.500000000000000444 ) ;
#5204=CARTESIAN_POINT ( 'NONE',  ( -4.140404888673278272, -2.228338276487456415, -3.686887068327035166 ) ) ;
#5276=CARTESIAN_POINT ( 'NONE',  ( 0.6937372685066666156, -4.453844082567737672, -3.610536846335894445 ) ) ;
#5286=ORIENTED_EDGE ( 'NONE', *, *, #6083, .F. ) ;
#5288=CARTESIAN_POINT ( 'NONE',  ( -4.207491450040567571, 2.029819825146470524, -3.671670828759566074 ) ) ;
#5376=EDGE_LOOP ( 'NONE', ( #10798, #40178, #5130, #15126, #16261 ) ) ;
#5407=CARTESIAN_POINT ( 'NONE',  ( 2.725741868436127202, -3.045094352033990148, -3.220599429844051453 ) ) ;
#5558=DIRECTION ( 'NONE',  ( -1.000000000000000000, 0.000000000000000000, 0.000000000000000000 ) ) ;
#5584=CARTESIAN_POINT ( 'NONE',  ( 2.682243648011666703, 3.070208061305304881, -0.04852650426601266831 ) ) ;
#5599=CARTESIAN_POINT ( 'NONE',  ( -6.259644161404862988E-16, -4.618802153517027165, -3.504271511726793076 ) ) ;
#5606=CARTESIAN_POINT ( 'NONE',  ( -2.687328764639638656, 3.067272167851286202, -0.05923475698270370959 ) ) ;
#5622=CARTESIAN_POINT ( 'NONE',  ( -0.6666666666666651864, 4.233901974057260098, -3.300726591567081147 ) ) ;
#5685=CARTESIAN_POINT ( 'NONE',  ( 0.000000000000000000, 0.000000000000000000, -5.000000000000000000 ) ) ;
#5704=CARTESIAN_POINT ( 'NONE',  ( -3.999999999998910649, -1.658469974638591804, -3.531532913075256186 ) ) ;
#5774=EDGE_CURVE ( 'NONE', #7155, #14112, #18026, .T. ) ;
#5790=CARTESIAN_POINT ( 'NONE',  ( 2.000000000000008882, 3.464101615137749945, 0.000000000000000000 ) ) ;
#5800=B_SPLINE_CURVE_WITH_KNOTS ( 'NONE', 3,
 ( #35503, #5622, #29203, #42470, #12616 ),
 .UNSPECIFIED., .F., .F.,
 ( 4, 1, 4 ),
 ( 0.000000000000000000, 0.002309401076758506657, 0.004618802153517013315 ),
 .UNSPECIFIED. ) ;
#6002=DIRECTION ( 'NONE',  ( -1.000000000000000000, 0.000000000000000000, 0.000000000000000000 ) ) ;
#6042=CARTESIAN_POINT ( 'NONE',  ( -1.654252653721913102, -3.663718938583024443, -0.01223254789874440342 ) ) ;
#6053=EDGE_CURVE ( 'NONE', #9725, #24319, #18827, .T. ) ;
#6083=EDGE_CURVE ( 'NONE', #22707, #20305, #12465, .T. ) ;
#6104=CARTESIAN_POINT ( 'NONE',  ( 8.673617379884035472E-16, 4.618802153517012954, -5.000000000000000000 ) ) ;
#6132=VERTEX_POINT ( 'NONE', #22510 ) ;
#6191=ORIENTED_EDGE ( 'NONE', *, *, #1218, .T. ) ;
#6210=VERTEX_POINT ( 'NONE', #13753 ) ;
#6223=ORIENTED_EDGE ( 'NONE', *, *, #29105, .F. ) ;
#6226=B_SPLINE_CURVE_WITH_KNOTS ( 'NONE', 3,
 ( #39101, #22163, #31948, #15389, #22791, #28683 ),
 .UNSPECIFIED., .F., .F.,
 ( 4, 2, 4 ),
 ( 0.002365888236228001588, 0.003551327329835089319, 0.004736766423442177049 ),
 .UNSPECIFIED. ) ;
#6252=ORIENTED_EDGE ( 'NONE', *, *, #29105, .T. ) ;
#6253=CARTESIAN_POINT ( 'NONE',  ( 0.000000000000000000, 0.000000000000000000, -5.000000000000000888 ) ) ;
#6272=CARTESIAN_POINT ( 'NONE',  ( -3.540020015735593439, -2.810662092924100630, -3.602146406945814672 ) ) ;
#6326=CIRCLE ( 'NONE', #36280, 4.000000000000000000 ) ;
#6370=EDGE_CURVE ( 'NONE', #33962, #3149, #8326, .T. ) ;
#6399=CARTESIAN_POINT ( 'NONE',  ( -4.000000000000000000, -2.309401076758512694, -3.433295621305382461 ) ) ;
#6469=CARTESIAN_POINT ( 'NONE',  ( -4.211140560182196957, -2.431303136016552013, -3.745885042887436178 ) ) ;
#6478=CARTESIAN_POINT ( 'NONE',  ( -0.5636800770129166693, -4.293361309317430319, -3.531542292955206275 ) ) ;
#6508=VECTOR ( 'NONE', #16715, 1000.000000000000000 ) ;
#6533=DIRECTION ( 'NONE',  ( -1.000000000000000000, 0.000000000000000000, 0.000000000000000000 ) ) ;
#6569=VERTEX_POINT ( 'NONE', #9058 ) ;
#6570=CLOSED_SHELL ( 'NONE', ( #17527, #8939, #18650, #17169, #651, #20611, #7454, #13247, #24876, #33588, #15300, #4190, #39708, #2307, #26676, #21432, #7158, #30137, #41052, #14137, #32648, #36567, #26012, #28588, #4566, #10564, #20823, #29772, #6626, #20715, #11503, #985 ) ) ;
#6624=B_SPLINE_CURVE_WITH_KNOTS ( 'NONE', 3,
 ( #18419, #41483, #11630, #8545, #5059, #5276, #18644, #2824 ),
 .UNSPECIFIED., .F., .F.,
 ( 4, 2, 2, 4 ),
 ( 0.000000000000000000, 0.002450665683189819262, 0.003675998524784728893, 0.004901331366379639391 ),
 .UNSPECIFIED. ) ;
#6626=ADVANCED_FACE ( 'NONE', ( #36508 ), #18509, .F. ) ;
#6675=ORIENTED_EDGE ( 'NONE', *, *, #7822, .T. ) ;
#6676=DIRECTION ( 'NONE',  ( -0.000000000000000000, -0.000000000000000000, 1.000000000000000000 ) ) ;
#6731=ORIENTED_EDGE ( 'NONE', *, *, #13712, .F. ) ;
#6763=DIRECTION ( 'NONE',  ( 0.000000000000000000, -1.000000000000000000, 0.000000000000000000 ) ) ;
#6791=DIRECTION ( 'NONE',  ( -1.000000000000000000, 0.000000000000000000, 0.000000000000000000 ) ) ;
#6847=ORIENTED_EDGE ( 'NONE', *, *, #15871, .T. ) ;
#6859=CARTESIAN_POINT ( 'NONE',  ( 0.000000000000000000, 0.000000000000000000, -5.000000000000000000 ) ) ;
#7066=AXIS2_PLACEMENT_3D ( 'NONE', #21707, #21915, #4635 ) ;
#7069=CARTESIAN_POINT ( 'NONE',  ( 0.6920835326022565237, 4.454600218803884459, -3.597382984111579862 ) ) ;
#7087=CARTESIAN_POINT ( 'NONE',  ( 4.000000000001088907, 1.658577278524410170, -3.531553309554541720 ) ) ;
#7155=VERTEX_POINT ( 'NONE', #33204 ) ;
#7158=ADVANCED_FACE ( 'NONE', ( #29951 ), #40184, .T. ) ;
#7238=EDGE_LOOP ( 'NONE', ( #24982, #23979, #34518, #26798 ) ) ;
#7273=CARTESIAN_POINT ( 'NONE',  ( 4.140404888673277384, 2.228338276487440428, -3.686887068327033390 ) ) ;
#7356=CARTESIAN_POINT ( 'NONE',  ( 2.000000000000005329, -3.464101615137751722, 0.000000000000000000 ) ) ;
#7370=DIRECTION ( 'NONE',  ( 0.8660254037844374864, -0.5000000000000018874, 0.000000000000000000 ) ) ;
#7424=ORIENTED_EDGE ( 'NONE', *, *, #6053, .T. ) ;
#7447=ORIENTED_EDGE ( 'NONE', *, *, #1044, .F. ) ;
#7454=ADVANCED_FACE ( 'NONE', ( #42327 ), #35762, .F. ) ;
#7501=CARTESIAN_POINT ( 'NONE',  ( 0.5636800770130377947, 4.293361309317166530, -3.531542292954102713 ) ) ;
#7546=CARTESIAN_POINT ( 'NONE',  ( -2.000000000000007550, -3.464101615137749945, 0.000000000000000000 ) ) ;
#7583=EDGE_CURVE ( 'NONE', #38985, #6569, #22346, .T. ) ;
#7662=VERTEX_POINT ( 'NONE', #1290 ) ;
#7696=ORIENTED_EDGE ( 'NONE', *, *, #2078, .F. ) ;
#7769=EDGE_CURVE ( 'NONE', #25462, #20305, #12887, .T. ) ;
#7822=EDGE_CURVE ( 'NONE', #39558, #6132, #10797, .T. ) ;
#7823=CARTESIAN_POINT ( 'NONE',  ( 3.999999999999999112, -0.7890432684750902093, -0.04868663549882291247 ) ) ;
#7828=CONICAL_SURFACE ( 'NONE', #36369, 2.500000000000000888, 0.9599310885968785900 ) ;
#7893=FACE_OUTER_BOUND ( 'NONE', #24021, .T. ) ;
#7918=LINE ( 'NONE', #25195, #20391 ) ;
#7947=EDGE_CURVE ( 'NONE', #29982, #27564, #6326, .T. ) ;
#8005=CARTESIAN_POINT ( 'NONE',  ( 1.411581201560190495E-15, 4.862606272033091592, -3.745885042887436622 ) ) ;
#8070=EDGE_CURVE ( 'NONE', #37442, #25462, #37820, .T. ) ;
#8125=CIRCLE ( 'NONE', #22092, 5.384454397937118664 ) ;
#8211=EDGE_CURVE ( 'NONE', #1657, #29146, #14446, .T. ) ;
#8253=CARTESIAN_POINT ( 'NONE',  ( 4.000000000000000000, 2.309401076758497151, -5.000000000000000000 ) ) ;
#8259=AXIS2_PLACEMENT_3D ( 'NONE', #41305, #11454, #16024 ) ;
#8326=B_SPLINE_CURVE_WITH_KNOTS ( 'NONE', 3,
 ( #17686, #40323, #30955, #24448, #24007 ),
 .UNSPECIFIED., .F., .F.,
 ( 4, 1, 4 ),
 ( 0.000000000000000000, 0.002309401076758505790, 0.004618802153517011580 ),
 .UNSPECIFIED. ) ;
#8337=CARTESIAN_POINT ( 'NONE',  ( 0.6666666666666689611, 4.233901974057261874, -3.300726591567082480 ) ) ;
#8466=FACE_BOUND ( 'NONE', #34394, .T. ) ;
#8479=CARTESIAN_POINT ( 'NONE',  ( -4.175002511812151873, -2.208363329454905877, -3.469254087858246738 ) ) ;
#8545=CARTESIAN_POINT ( 'NONE',  ( 1.747541505913279281, -3.837784562140273081, -3.503702292528912299 ) ) ;
#8552=CARTESIAN_POINT ( 'NONE',  ( -4.211405944401398038, -2.460460786169389902, -3.751298493805494072 ) ) ;
#8576=ORIENTED_EDGE ( 'NONE', *, *, #4895, .T. ) ;
#8623=CIRCLE ( 'NONE', #40645, 2.500000000000000444 ) ;
#8634=VECTOR ( 'NONE', #15954, 999.9999999999998863 ) ;
#8650=DIRECTION ( 'NONE',  ( 0.000000000000000000, 0.000000000000000000, 1.000000000000000000 ) ) ;
#8805=CONICAL_SURFACE ( 'NONE', #37358, 5.560781378645573980, 1.221730476396046816 ) ;
#8869=ORIENTED_EDGE ( 'NONE', *, *, #31908, .T. ) ;
#8939=ADVANCED_FACE ( 'NONE', ( #20994 ), #7828, .F. ) ;
#8949=EDGE_LOOP ( 'NONE', ( #7447, #6847, #42498, #30414, #33820 ) ) ;
#9058=CARTESIAN_POINT ( 'NONE',  ( -4.211140560182196957, -2.431303136016552013, -3.745885042887436178 ) ) ;
#9306=CARTESIAN_POINT ( 'NONE',  ( 1.999999999999998224, -3.464101615137772594, -3.142992957459239012 ) ) ;
#9320=ORIENTED_EDGE ( 'NONE', *, *, #15309, .T. ) ;
#9327=ORIENTED_EDGE ( 'NONE', *, *, #42887, .F. ) ;
#9366=CARTESIAN_POINT ( 'NONE',  ( 4.101954839143059139, -2.368264730582948285, -3.681130640444269631 ) ) ;
#9379=VECTOR ( 'NONE', #2939, 1000.000000000000000 ) ;
#9438=EDGE_CURVE ( 'NONE', #31862, #7662, #39172, .T. ) ;
#9514=CARTESIAN_POINT ( 'NONE',  ( 4.000000000000000000, -2.511475576507276042, -3.469253905236643565 ) ) ;
#9621=ORIENTED_EDGE ( 'NONE', *, *, #16089, .F. ) ;
#9671=DIRECTION ( 'NONE',  ( -0.000000000000000000, -0.000000000000000000, 1.000000000000000000 ) ) ;
#9683=ORIENTED_EDGE ( 'NONE', *, *, #8070, .T. ) ;
#9725=VERTEX_POINT ( 'NONE', #42654 ) ;
#9741=CARTESIAN_POINT ( 'NONE',  ( -3.511755186886750479, 2.826662030176366081, -3.597382984111578086 ) ) ;
#9742=CARTESIAN_POINT ( 'NONE',  ( 3.333333333333335702, -2.694301256218268215, -3.300726591567084256 ) ) ;
#9802=CARTESIAN_POINT ( 'NONE',  ( 0.000000000000000000, 0.000000000000000000, -5.000000000000000888 ) ) ;
#9971=ORIENTED_EDGE ( 'NONE', *, *, #32896, .F. ) ;
#9973=CARTESIAN_POINT ( 'NONE',  ( 0.02511973781850649831, -4.877415612947427981, -3.751298745799844792 ) ) ;
#10003=ORIENTED_EDGE ( 'NONE', *, *, #7583, .F. ) ;
#10080=AXIS2_PLACEMENT_3D ( 'NONE', #30663, #1611, #31524 ) ;
#10086=EDGE_LOOP ( 'NONE', ( #26281, #3736, #1474 ) ) ;
#10120=CARTESIAN_POINT ( 'NONE',  ( 2.836893136758676270, 3.208949435745843903, -3.505054077164911241 ) ) ;
#10213=DIRECTION ( 'NONE',  ( 1.000000000000000000, 0.000000000000000000, 0.000000000000000000 ) ) ;
#10246=( NAMED_UNIT ( * ) PLANE_ANGLE_UNIT ( ) SI_UNIT ( $, .RADIAN. ) );
#10270=CARTESIAN_POINT ( 'NONE',  ( 4.000000000000000000, -2.309401076758516691, -0.4999999999999995559 ) ) ;
#10348=EDGE_CURVE ( 'NONE', #33962, #15592, #27146, .T. ) ;
#10377=CARTESIAN_POINT ( 'NONE',  ( 4.203935335434060505, 1.640780671294165272, -3.598452447879202598 ) ) ;
#10424=EDGE_CURVE ( 'NONE', #3149, #22707, #13220, .T. ) ;
#10427=CARTESIAN_POINT ( 'NONE',  ( 2.345747346278113987, -3.264484291692503870, -0.01223254789874484924 ) ) ;
#10430=CARTESIAN_POINT ( 'NONE',  ( -1.317756351988340180, 3.857995168970202116, -0.04852650426601388955 ) ) ;
#10474=DIRECTION ( 'NONE',  ( 0.000000000000000000, 0.000000000000000000, -1.000000000000000000 ) ) ;
#10478=DIRECTION ( 'NONE',  ( -1.000000000000000000, 0.000000000000000000, 0.000000000000000000 ) ) ;
#10564=ADVANCED_FACE ( 'NONE', ( #31271 ), #36281, .F. ) ;
#10565=CARTESIAN_POINT ( 'NONE',  ( -0.02511973781850462134, 4.877415612947412882, -3.751298745799839462 ) ) ;
#10581=DIRECTION ( 'NONE',  ( -1.000000000000000000, 0.000000000000000000, 0.000000000000000000 ) ) ;
#10691=CARTESIAN_POINT ( 'NONE',  ( 3.999999999999999112, 1.941961291383486277, -0.3515519931180248192 ) ) ;
#10732=CARTESIAN_POINT ( 'NONE',  ( 0.000000000000000000, 0.000000000000000000, 0.000000000000000000 ) ) ;
#10760=ORIENTED_EDGE ( 'NONE', *, *, #36221, .F. ) ;
#10783=CARTESIAN_POINT ( 'NONE',  ( 0.5449313310647804220, 4.304185902836899835, -3.316620875263383894 ) ) ;
#10797=B_SPLINE_CURVE_WITH_KNOTS ( 'NONE', 3,
 ( #22276, #16338, #29644, #42696 ),
 .UNSPECIFIED., .F., .F.,
 ( 4, 4 ),
 ( 0.000000000000000000, 0.002452478801916361129 ),
 .UNSPECIFIED. ) ;
#10798=ORIENTED_EDGE ( 'NONE', *, *, #10348, .F. ) ;
#10808=AXIS2_PLACEMENT_3D ( 'NONE', #2000, #38435, #22759 ) ;
#10996=CARTESIAN_POINT ( 'NONE',  ( -4.000000000000000000, 2.511478553582031203, -3.469254451724764543 ) ) ;
#10997=EDGE_CURVE ( 'NONE', #15592, #17801, #95, .T. ) ;
#11032=CARTESIAN_POINT ( 'NONE',  ( 1.567478505476134606E-15, 4.618802153517012066, -3.433295621305382905 ) ) ;
#11039=AXIS2_PLACEMENT_3D ( 'NONE', #11341, #40982, #11133 ) ;
#11058=DIRECTION ( 'NONE',  ( 0.000000000000000000, 0.000000000000000000, 1.000000000000000000 ) ) ;
#11133=DIRECTION ( 'NONE',  ( 1.000000000000000000, 0.000000000000000000, 0.000000000000000000 ) ) ;
#11138=CARTESIAN_POINT ( 'NONE',  ( 0.3208286057739604957, -4.433571671609698228, -0.3503314178412692548 ) ) ;
#11188=DIRECTION ( 'NONE',  ( -1.000000000000000000, 0.000000000000000000, 0.000000000000000000 ) ) ;
#11193=CARTESIAN_POINT ( 'NONE',  ( -3.436319922987618902, 2.634841920961291439, -3.531542292955721862 ) ) ;
#11201=VERTEX_POINT ( 'NONE', #24153 ) ;
#11212=CARTESIAN_POINT ( 'NONE',  ( -4.197393957002303999, 0.4069871074557429025, -3.503767560748926257 ) ) ;
#11226=ORIENTED_EDGE ( 'NONE', *, *, #4759, .T. ) ;
#11245=CARTESIAN_POINT ( 'NONE',  ( -2.500000000000000888, 0.000000000000000000, -4.974599999999998801 ) ) ;
#11321=CARTESIAN_POINT ( 'NONE',  ( 3.436319922986518449, -2.634841920959471562, -3.531542292954761741 ) ) ;
#11341=CARTESIAN_POINT ( 'NONE',  ( 0.000000000000000000, 0.000000000000000000, -0.3080913168122742518 ) ) ;
#11354=CARTESIAN_POINT ( 'NONE',  ( -4.000000000000000000, -0.7890432684750890990, -0.04868663549882315533 ) ) ;
#11403=CARTESIAN_POINT ( 'NONE',  ( -0.5469614295416921346, 4.303013824936271270, -3.535263753543735454 ) ) ;
#11454=DIRECTION ( 'NONE',  ( 0.000000000000000000, 0.000000000000000000, -1.000000000000000000 ) ) ;
#11503=ADVANCED_FACE ( 'NONE', ( #33860 ), #14805, .F. ) ;
#11533=DIRECTION ( 'NONE',  ( 0.000000000000000000, 0.000000000000000000, 1.000000000000000000 ) ) ;
#11596=AXIS2_PLACEMENT_3D ( 'NONE', #371, #33126, #7370 ) ;
#11630=CARTESIAN_POINT ( 'NONE',  ( 2.805705207896068476, -3.226868319750173075, -3.503898532754370354 ) ) ;
#11644=CARTESIAN_POINT ( 'NONE',  ( 4.204015924366189871, -1.626724848190933548, -3.610627190413393084 ) ) ;
#11672=DIRECTION ( 'NONE',  ( -0.000000000000000000, -0.000000000000000000, 1.000000000000000000 ) ) ;
#11689=ORIENTED_EDGE ( 'NONE', *, *, #34406, .T. ) ;
#11701=DIRECTION ( 'NONE',  ( 1.000000000000000000, 0.000000000000000000, 0.000000000000000000 ) ) ;
#11745=CONICAL_SURFACE ( 'NONE', #20822, 4.000000000000000000, 0.8911886515913786111 ) ;
#11845=CARTESIAN_POINT ( 'NONE',  ( 0.1404048886732821022, 4.699864953788070565, -3.686887068327037387 ) ) ;
#11863=CARTESIAN_POINT ( 'NONE',  ( 4.197393957002303999, 7.772902908466098641E-14, -3.503767560748929810 ) ) ;
#11903=AXIS2_PLACEMENT_3D ( 'NONE', #6253, #28771, #42249 ) ;
#11914=AXIS2_PLACEMENT_3D ( 'NONE', #5685, #29265, #43179 ) ;
#11937=VECTOR ( 'NONE', #36487, 1000.000000000000000 ) ;
#12038=CARTESIAN_POINT ( 'NONE',  ( -6.259644161404860030E-16, -4.618802153517027165, -5.000000000000000000 ) ) ;
#12145=ORIENTED_EDGE ( 'NONE', *, *, #20444, .F. ) ;
#12170=CARTESIAN_POINT ( 'NONE',  ( -1.240299975428134203E-15, -4.736529461165891242, -3.681130640444276292 ) ) ;
#12179=CARTESIAN_POINT ( 'NONE',  ( -3.680118525130244400, 2.494084732383327285, -0.3507732604232449702 ) ) ;
#12256=MECHANICAL_DESIGN_GEOMETRIC_PRESENTATION_REPRESENTATION('',(#25519),#39405);
#12271=CARTESIAN_POINT ( 'NONE',  ( 1.567478505476134606E-15, 4.618802153517012066, -3.433295621305382905 ) ) ;
#12465=LINE ( 'NONE', #12038, #32090 ) ;
#12499=ORIENTED_EDGE ( 'NONE', *, *, #30016, .T. ) ;
#12505=DIRECTION ( 'NONE',  ( 1.000000000000000000, 0.000000000000000000, 0.000000000000000000 ) ) ;
#12525=FILL_AREA_STYLE_COLOUR ( '', #3862 ) ;
#12549=CARTESIAN_POINT ( 'NONE',  ( -4.000000000000000000, 2.309401076758498483, -5.000000000000000000 ) ) ;
#12616=CARTESIAN_POINT ( 'NONE',  ( -4.000000000000000000, 2.309401076758498483, -3.433295621305379353 ) ) ;
#12619=EDGE_CURVE ( 'NONE', #7155, #26591, #6226, .T. ) ;
#12629=CARTESIAN_POINT ( 'NONE',  ( -1.287237434361707233, -3.875615274277397937, -3.430618716626816500 ) ) ;
#12638=ORIENTED_EDGE ( 'NONE', *, *, #32299, .T. ) ;
#12773=CARTESIAN_POINT ( 'NONE',  ( -5.560781378645573980, 0.000000000000000000, -4.000000000000000000 ) ) ;
#12880=CARTESIAN_POINT ( 'NONE',  ( 4.211140560182196957, -2.431303136016555122, -3.745885042887436622 ) ) ;
#12887=B_SPLINE_CURVE_WITH_KNOTS ( 'NONE', 3,
 ( #40991, #31848, #1934, #25325, #11138, #31418 ),
 .UNSPECIFIED., .F., .F.,
 ( 4, 2, 4 ),
 ( 0.002365888236227967761, 0.003551327329835077609, 0.004736766423442186590 ),
 .UNSPECIFIED. ) ;
#13008=LINE ( 'NONE', #27380, #34588 ) ;
#13056=ORIENTED_EDGE ( 'NONE', *, *, #29273, .F. ) ;
#13202=FACE_OUTER_BOUND ( 'NONE', #26953, .T. ) ;
#13213=CARTESIAN_POINT ( 'NONE',  ( 4.235886605889389145, 2.417314728048528760, -3.751161874094018245 ) ) ;
#13220=B_SPLINE_CURVE_WITH_KNOTS ( 'NONE', 3,
 ( #6399, #20192, #20398, #19746, #33657 ),
 .UNSPECIFIED., .F., .F.,
 ( 4, 1, 4 ),
 ( 0.000000000000000000, 0.002309401076758505356, 0.004618802153517010713 ),
 .UNSPECIFIED. ) ;
#13241=EDGE_CURVE ( 'NONE', #19145, #33962, #23954, .T. ) ;
#13247=ADVANCED_FACE ( 'NONE', ( #4280 ), #20486, .T. ) ;
#13313=LINE ( 'NONE', #26604, #32473 ) ;
#13497=ORIENTED_EDGE ( 'NONE', *, *, #39998, .T. ) ;
#13552=AXIS2_PLACEMENT_3D ( 'NONE', #3852, #14597, #10213 ) ;
#13585=ORIENTED_EDGE ( 'NONE', *, *, #26227, .T. ) ;
#13643=CARTESIAN_POINT ( 'NONE',  ( 1.274258131564866448, 3.883108878240963513, -3.220599429844046568 ) ) ;
#13712=EDGE_CURVE ( 'NONE', #1657, #39558, #24429, .T. ) ;
#13743=CARTESIAN_POINT ( 'NONE',  ( 4.000000000000000000, -1.084202172485504434E-14, -3.142992957459231906 ) ) ;
#13753=CARTESIAN_POINT ( 'NONE',  ( -4.197393957002303999, -7.773935952363655451E-14, -3.503767560748929810 ) ) ;
#13801=ORIENTED_EDGE ( 'NONE', *, *, #33405, .F. ) ;
#13803=PLANE ( 'NONE',  #29021 ) ;
#13807=ORIENTED_EDGE ( 'NONE', *, *, #39418, .F. ) ;
#13818=CONICAL_SURFACE ( 'NONE', #11039, 2.059999999999998721, 0.9599310885968738161 ) ;
#13855=EDGE_LOOP ( 'NONE', ( #38370, #28080, #33278, #29803, #22932 ) ) ;
#13921=CARTESIAN_POINT ( 'NONE',  ( -4.197393957002303999, -0.8151795401431414234, -3.503767560748935139 ) ) ;
#13936=CARTESIAN_POINT ( 'NONE',  ( 2.171643655288379993, -3.365003104552334978, -1.195831703456429434E-14 ) ) ;
#14047=EDGE_LOOP ( 'NONE', ( #6675, #31962, #8576, #14913, #13497, #34580, #35866 ) ) ;
#14104=CARTESIAN_POINT ( 'NONE',  ( 4.197310751797292738, 0.8178363989516252985, -3.502498386812444409 ) ) ;
#14112=VERTEX_POINT ( 'NONE', #17535 ) ;
#14137=ADVANCED_FACE ( 'NONE', ( #460 ), #15110, .T. ) ;
#14159=DIRECTION ( 'NONE',  ( -1.000000000000000000, 0.000000000000000000, 0.000000000000000000 ) ) ;
#14263=CARTESIAN_POINT ( 'NONE',  ( -4.197312064133472020, -0.8182229787990021874, -3.502518405183886685 ) ) ;
#14310=CARTESIAN_POINT ( 'NONE',  ( 0.000000000000000000, 0.000000000000000000, 0.000000000000000000 ) ) ;
#14327=PLANE ( 'NONE',  #32439 ) ;
#14356=CARTESIAN_POINT ( 'NONE',  ( -4.211140560182196957, 2.431303136016537803, -3.745885042887433514 ) ) ;
#14446=B_SPLINE_CURVE_WITH_KNOTS ( 'NONE', 3,
 ( #8005, #31152, #34398, #1241, #4954, #15019 ),
 .UNSPECIFIED., .F., .F.,
 ( 4, 2, 4 ),
 ( -3.640115492407174633E-06, 0.0002066546034006553863, 0.0004169493222937179812 ),
 .UNSPECIFIED. ) ;
#14478=AXIS2_PLACEMENT_3D ( 'NONE', #23490, #40446, #10581 ) ;
#14499=CARTESIAN_POINT ( 'NONE',  ( 0.000000000000000000, 0.000000000000000000, 0.000000000000000000 ) ) ;
#14547=CARTESIAN_POINT ( 'NONE',  ( -4.000000000000000000, 0.1981133338132459731, 2.096406544454392723E-17 ) ) ;
#14590=CARTESIAN_POINT ( 'NONE',  ( -1.655952806101422814, 3.662737355149034979, -7.623296525288699970E-18 ) ) ;
#14597=DIRECTION ( 'NONE',  ( 0.000000000000000000, 0.000000000000000000, 1.000000000000000000 ) ) ;
#14639=VERTEX_POINT ( 'NONE', #27434 ) ;
#14742=AXIS2_PLACEMENT_3D ( 'NONE', #23929, #30039, #37197 ) ;
#14774=EDGE_CURVE ( 'NONE', #27564, #25474, #14991, .T. ) ;
#14793=ORIENTED_EDGE ( 'NONE', *, *, #7769, .T. ) ;
#14803=CYLINDRICAL_SURFACE ( 'NONE', #31303, 2.100000000000000089 ) ;
#14805=CONICAL_SURFACE ( 'NONE', #26646, 2.500000000000000888, 0.9599310885968785900 ) ;
#14844=FACE_OUTER_BOUND ( 'NONE', #29335, .T. ) ;
#14894=AXIS2_PLACEMENT_3D ( 'NONE', #24166, #18284, #31549 ) ;
#14906=CARTESIAN_POINT ( 'NONE',  ( -1.360585162435467455, 4.061296242128285883, -3.505054077164959203 ) ) ;
#14911=ORIENTED_EDGE ( 'NONE', *, *, #30113, .F. ) ;
#14913=ORIENTED_EDGE ( 'NONE', *, *, #26227, .F. ) ;
#14991=B_SPLINE_CURVE_WITH_KNOTS ( 'NONE', 3,
 ( #5790, #19146, #5584, #15642, #25071, #28739 ),
 .UNSPECIFIED., .F., .F.,
 ( 4, 2, 4 ),
 ( 0.002365888236227995517, 0.003551327329835084114, 0.004736766423442172712 ),
 .UNSPECIFIED. ) ;
#15019=CARTESIAN_POINT ( 'NONE',  ( 1.567478505476134606E-15, 4.618802153517012066, -3.433295621305382905 ) ) ;
#15030=LINE ( 'NONE', #39176, #9379 ) ;
#15041=CARTESIAN_POINT ( 'NONE',  ( -0.1750025118121544265, -4.719839900820635314, -3.469254087858253399 ) ) ;
#15110=CONICAL_SURFACE ( 'NONE', #26944, 4.000000000000000000, 0.8911886515913786111 ) ;
#15126=ORIENTED_EDGE ( 'NONE', *, *, #36221, .T. ) ;
#15147=CARTESIAN_POINT ( 'NONE',  ( -4.000000000000000000, -0.8382240730041925492, -3.220610619767135141 ) ) ;
#15151=CARTESIAN_POINT ( 'NONE',  ( -4.198928548860774157, 0.8158838809860065044, -3.526471437616918170 ) ) ;
#15183=DIRECTION ( 'NONE',  ( 0.5000000000000013323, -0.8660254037844379305, 0.000000000000000000 ) ) ;
#15200=ORIENTED_EDGE ( 'NONE', *, *, #42423, .F. ) ;
#15210=CARTESIAN_POINT ( 'NONE',  ( -4.000000000000000000, 2.309401076758498483, -0.4999999999999927280 ) ) ;
#15225=AXIS2_PLACEMENT_3D ( 'NONE', #24879, #25298, #38129 ) ;
#15261=CARTESIAN_POINT ( 'NONE',  ( -6.473970235329672780E-16, -4.862606272033106691, -3.745885042887442395 ) ) ;
#15300=ADVANCED_FACE ( 'NONE', ( #31517 ), #31727, .T. ) ;
#15309=EDGE_CURVE ( 'NONE', #29305, #9725, #17358, .T. ) ;
#15389=CARTESIAN_POINT ( 'NONE',  ( -3.349226789952655547, -2.685125164760744809, -0.2236248678334863682 ) ) ;
#15406=ORIENTED_EDGE ( 'NONE', *, *, #32896, .T. ) ;
#15415=CARTESIAN_POINT ( 'NONE',  ( 4.211140560182196957, 2.431303136016536470, -3.745885042887433514 ) ) ;
#15429=LINE ( 'NONE', #26717, #6508 ) ;
#15435=AXIS2_PLACEMENT_3D ( 'NONE', #38486, #4912, #11701 ) ;
#15452=ORIENTED_EDGE ( 'NONE', *, *, #15937, .T. ) ;
#15455=FACE_OUTER_BOUND ( 'NONE', #23729, .T. ) ;
#15486=LINE ( 'NONE', #28362, #29570 ) ;
#15592=VERTEX_POINT ( 'NONE', #19962 ) ;
#15642=CARTESIAN_POINT ( 'NONE',  ( 3.349226789952652439, 2.685125164760731487, -0.2236248678334773199 ) ) ;
#15734=CARTESIAN_POINT ( 'NONE',  ( 4.000000000000000000, -2.309401076758514915, -3.433295621305383349 ) ) ;
#15806=CARTESIAN_POINT ( 'NONE',  ( -6.259644161404860030E-16, -4.618802153517027165, -5.000000000000000000 ) ) ;
#15871=EDGE_CURVE ( 'NONE', #28956, #29146, #24335, .T. ) ;
#15929=ORIENTED_EDGE ( 'NONE', *, *, #26695, .T. ) ;
#15937=EDGE_CURVE ( 'NONE', #11201, #38985, #6624, .T. ) ;
#15954=DIRECTION ( 'NONE',  ( 0.8191520442889875797, 0.000000000000000000, 0.5735764363510522656 ) ) ;
#16020=AXIS2_PLACEMENT_3D ( 'NONE', #20125, #6763, #414 ) ;
#16024=DIRECTION ( 'NONE',  ( 1.000000000000000000, 0.000000000000000000, 0.000000000000000000 ) ) ;
#16089=EDGE_CURVE ( 'NONE', #3149, #26591, #23178, .T. ) ;
#16207=DIRECTION ( 'NONE',  ( -0.000000000000000000, 0.000000000000000000, -1.000000000000000000 ) ) ;
#16261=ORIENTED_EDGE ( 'NONE', *, *, #39576, .T. ) ;
#16265=DIRECTION ( 'NONE',  ( -0.9396926207859138680, 0.000000000000000000, -0.3420201433256536139 ) ) ;
#16338=CARTESIAN_POINT ( 'NONE',  ( 4.203833317240879275, 1.627343821129582979, -3.597273115243889929 ) ) ;
#16430=ORIENTED_EDGE ( 'NONE', *, *, #29509, .F. ) ;
#16555=CARTESIAN_POINT ( 'NONE',  ( -4.197393957002303999, -7.773935952363655451E-14, -3.503767560748929810 ) ) ;
#16587=( BOUNDED_SURFACE ( )  B_SPLINE_SURFACE ( 3, 2, ( 
 ( #31033, #11845, #4615 ),
 ( #35151, #11403, #25172 ),
 ( #34292, #1342, #14906 ),
 ( #24967, #27785, #41041 ),
 ( #38215, #11193, #4842 ),
 ( #37775, #38420, #34735 ) ),
 .UNSPECIFIED., .F., .F., .T. ) 
 B_SPLINE_SURFACE_WITH_KNOTS ( ( 4, 2, 4 ),
 ( 3, 3 ),
 ( 0.02032853247518125531, 0.02278863295364820865, 0.02524873343211516200 ),
 ( 0.000000000000000000, 1.000000000000000000 ),
 .UNSPECIFIED. ) 
 GEOMETRIC_REPRESENTATION_ITEM ( )  RATIONAL_B_SPLINE_SURFACE ( (
 ( 1.000000000000000000, 0.8047781615896836271, 1.000000000000000000),
 ( 1.000000000000000000, 0.8123767586289967202, 1.000000000000000000),
 ( 1.000000000000000000, 0.8190662415563443322, 1.000000000000000000),
 ( 1.000000000000000000, 0.8192361015669982205, 1.000000000000000000),
 ( 1.000000000000000000, 0.8126135807103181952, 1.000000000000000000),
 ( 1.000000000000000000, 0.8047712338318587788, 1.000000000000000000) ) ) 
 REPRESENTATION_ITEM ( '' )  SURFACE ( )  );
#16594=CARTESIAN_POINT ( 'NONE',  ( 5.560781378645575757, 0.000000000000000000, -4.000000000000000000 ) ) ;
#16640=ORIENTED_EDGE ( 'NONE', *, *, #29729, .F. ) ;
#16715=DIRECTION ( 'NONE',  ( -0.000000000000000000, -0.000000000000000000, 1.000000000000000000 ) ) ;
#16943=EDGE_CURVE ( 'NONE', #6569, #6210, #20990, .T. ) ;
#17037=AXIS2_PLACEMENT_3D ( 'NONE', #6104, #25979, #3232 ) ;
#17169=ADVANCED_FACE ( 'NONE', ( #18735 ), #8805, .T. ) ;
#17287=CARTESIAN_POINT ( 'NONE',  ( -4.000000000000000000, -0.3979232138631226823, -3.896351557369779711E-17 ) ) ;
#17311=EDGE_CURVE ( 'NONE', #1858, #880, #8125, .T. ) ;
#17358=CIRCLE ( 'NONE', #8259, 2.100000000000000089 ) ;
#17363=DIRECTION ( 'NONE',  ( 0.000000000000000000, 0.000000000000000000, 1.000000000000000000 ) ) ;
#17476=ORIENTED_EDGE ( 'NONE', *, *, #12619, .F. ) ;
#17486=CARTESIAN_POINT ( 'NONE',  ( -2.449848172108560540, -3.432307619358754724, -3.503702292528910078 ) ) ;
#17492=EDGE_CURVE ( 'NONE', #20680, #35337, #13008, .T. ) ;
#17527=ADVANCED_FACE ( 'NONE', ( #31076 ), #1167, .F. ) ;
#17535=CARTESIAN_POINT ( 'NONE',  ( -4.000000000000000000, 0.000000000000000000, 0.000000000000000000 ) ) ;
#17589=CARTESIAN_POINT ( 'NONE',  ( 2.804994570502171047, 3.229033611042449792, -3.526374918436834704 ) ) ;
#17652=CARTESIAN_POINT ( 'NONE',  ( -4.000000000000004441, 2.309401076758496263, -3.504269196027523847 ) ) ;
#17661=CARTESIAN_POINT ( 'NONE',  ( -0.6507732100473471171, 4.243078065514775510, -0.2236248678334823436 ) ) ;
#17686=CARTESIAN_POINT ( 'NONE',  ( -4.000000000000000000, 2.309401076758498483, -3.433295621305379353 ) ) ;
#17702=CARTESIAN_POINT ( 'NONE',  ( -0.6920835326022555245, -4.454600218803899558, -3.597382984111586079 ) ) ;
#17764=B_SPLINE_CURVE_WITH_KNOTS ( 'NONE', 3,
 ( #22660, #23297, #9306, #9742, #2737 ),
 .UNSPECIFIED., .F., .F.,
 ( 4, 1, 4 ),
 ( 5.640274452250024914E-20, 0.002309401076758505356, 0.004618802153517010713 ),
 .UNSPECIFIED. ) ;
#17801=VERTEX_POINT ( 'NONE', #32146 ) ;
#17829=CARTESIAN_POINT ( 'NONE',  ( -4.000000000000000000, 0.7924765000094600165, -0.05906175389889745803 ) ) ;
#17914=CARTESIAN_POINT ( 'NONE',  ( 3.999999999999999112, -0.3979232138631231819, -5.929230630780099908E-17 ) ) ;
#18026=CIRCLE ( 'NONE', #2588, 4.000000000000000000 ) ;
#18165=ORIENTED_EDGE ( 'NONE', *, *, #7822, .F. ) ;
#18284=DIRECTION ( 'NONE',  ( 0.000000000000000000, 0.000000000000000000, -1.000000000000000000 ) ) ;
#18382=DIRECTION ( 'NONE',  ( -0.000000000000000000, -0.000000000000000000, 1.000000000000000000 ) ) ;
#18419=CARTESIAN_POINT ( 'NONE',  ( 4.211140560182196957, -2.431303136016555122, -3.745885042887436622 ) ) ;
#18482=CARTESIAN_POINT ( 'NONE',  ( -4.000000000000000000, 0.000000000000000000, 0.000000000000000000 ) ) ;
#18509=( BOUNDED_SURFACE ( )  B_SPLINE_SURFACE ( 3, 2, ( 
 ( #40218, #7273, #13213 ),
 ( #27371, #271, #3553 ),
 ( #33678, #39988, #10120 ),
 ( #13643, #23471, #37163 ),
 ( #10783, #7501, #36735 ),
 ( #512, #34119, #10565 ) ),
 .UNSPECIFIED., .F., .F., .F. ) 
 B_SPLINE_SURFACE_WITH_KNOTS ( ( 4, 2, 4 ),
 ( 3, 3 ),
 ( 0.02032853247518126225, 0.02278863295364821212, 0.02524873343211516200 ),
 ( 0.000000000000000000, 1.000000000000000000 ),
 .UNSPECIFIED. ) 
 GEOMETRIC_REPRESENTATION_ITEM ( )  RATIONAL_B_SPLINE_SURFACE ( (
 ( 1.000000000000000000, 0.8047781615896835161, 1.000000000000000000),
 ( 1.000000000000000000, 0.8123767586291043008, 1.000000000000000000),
 ( 1.000000000000000000, 0.8190662415562011134, 1.000000000000000000),
 ( 1.000000000000000000, 0.8192361015671398849, 1.000000000000000000),
 ( 1.000000000000000000, 0.8126135807102121689, 1.000000000000000000),
 ( 1.000000000000000000, 0.8047712338318585568, 1.000000000000000000) ) ) 
 REPRESENTATION_ITEM ( '' )  SURFACE ( )  );
#18534=ORIENTED_EDGE ( 'NONE', *, *, #1960, .F. ) ;
#18537=EDGE_LOOP ( 'NONE', ( #25170, #29917, #23012 ) ) ;
#18547=CARTESIAN_POINT ( 'NONE',  ( 1.257172072275274388, -3.892973519170983110, -3.433252694550781303 ) ) ;
#18567=CARTESIAN_POINT ( 'NONE',  ( -4.235886605889389145, -2.417314728048544303, -3.751161874094020909 ) ) ;
#18644=CARTESIAN_POINT ( 'NONE',  ( 0.3461262719736147297, -4.658553426539303821, -3.671615880910379381 ) ) ;
#18650=ADVANCED_FACE ( 'NONE', ( #41193 ), #13818, .F. ) ;
#18653=CARTESIAN_POINT ( 'NONE',  ( -4.000000000000000000, -2.472261339043343220, -3.687027428081192326 ) ) ;
#18661=CARTESIAN_POINT ( 'NONE',  ( 4.207491450040567571, -2.029819825146485179, -3.671670828759567407 ) ) ;
#18678=ORIENTED_EDGE ( 'NONE', *, *, #15937, .F. ) ;
#18735=FACE_OUTER_BOUND ( 'NONE', #14047, .T. ) ;
#18748=CIRCLE ( 'NONE', #32605, 4.000000000000000000 ) ;
#18772=B_SPLINE_CURVE_WITH_KNOTS ( 'NONE', 3,
 ( #15734, #19234, #39885, #9366, #39676, #12880 ),
 .UNSPECIFIED., .F., .F.,
 ( 4, 2, 4 ),
 ( 4.336808689942017736E-19, 0.0002095117440854729585, 0.0004190234881709454834 ),
 .UNSPECIFIED. ) ;
#18775=CARTESIAN_POINT ( 'NONE',  ( 4.236525694536557474, -2.416953475386482530, -3.751298745799839462 ) ) ;
#18827=LINE ( 'NONE', #19026, #8634 ) ;
#18852=CARTESIAN_POINT ( 'NONE',  ( 3.333333333333332593, 2.694301256218250007, -3.300726591567078483 ) ) ;
#18890=( LENGTH_UNIT ( ) NAMED_UNIT ( * ) SI_UNIT ( .MILLI., .METRE. ) );
#18916=DIRECTION ( 'NONE',  ( 0.000000000000000000, 0.000000000000000000, 1.000000000000000000 ) ) ;
#18981=CARTESIAN_POINT ( 'NONE',  ( 8.673617379884035472E-16, 4.618802153517012954, 0.000000000000000000 ) ) ;
#19026=CARTESIAN_POINT ( 'NONE',  ( 2.059999999999998721, 0.000000000000000000, -0.3080913168122742518 ) ) ;
#19052=ORIENTED_EDGE ( 'NONE', *, *, #13241, .F. ) ;
#19145=VERTEX_POINT ( 'NONE', #21311 ) ;
#19146=CARTESIAN_POINT ( 'NONE',  ( 2.344047193898588954, 3.265465875126468021, -5.031375706690542042E-16 ) ) ;
#19179=CARTESIAN_POINT ( 'NONE',  ( -1.312671235360383548, -3.860931062424228788, -0.05923475698271369466 ) ) ;
#19183=CARTESIAN_POINT ( 'NONE',  ( -4.154094228333736538, -2.398367420967545627, -3.721909803043222276 ) ) ;
#19234=CARTESIAN_POINT ( 'NONE',  ( 4.000000000000003553, -2.309401076758513138, -3.504271511726786859 ) ) ;
#19284=( NAMED_UNIT ( * ) PLANE_ANGLE_UNIT ( ) SI_UNIT ( $, .RADIAN. ) );
#19298=SURFACE_SIDE_STYLE ('',( #43175 ) ) ;
#19472=ORIENTED_EDGE ( 'NONE', *, *, #2560, .T. ) ;
#19483=CARTESIAN_POINT ( 'NONE',  ( -4.000000000000000000, -2.512220745329312610, -3.469390707569719901 ) ) ;
#19497=( NAMED_UNIT ( * ) SI_UNIT ( $, .STERADIAN. ) SOLID_ANGLE_UNIT ( ) );
#19514=CIRCLE ( 'NONE', #16020, 0.5155456020628804703 ) ;
#19593=CARTESIAN_POINT ( 'NONE',  ( -1.393927851585477606, 4.043713361053528743, -3.526374918436835149 ) ) ;
#19601=CARTESIAN_POINT ( 'NONE',  ( -4.024497503033519941, -2.323544716729390558, -3.572167766733381544 ) ) ;
#19623=CARTESIAN_POINT ( 'NONE',  ( 4.211140560182196957, 2.431303136016536470, -3.745885042887433514 ) ) ;
#19746=CARTESIAN_POINT ( 'NONE',  ( -0.6666666666666666297, -4.233901974057276973, -3.300726591567087365 ) ) ;
#19752=DIRECTION ( 'NONE',  ( 0.000000000000000000, 0.000000000000000000, -1.000000000000000000 ) ) ;
#19775=DIRECTION ( 'NONE',  ( 1.000000000000000000, 0.000000000000000000, 0.000000000000000000 ) ) ;
#19777=VECTOR ( 'NONE', #16265, 1000.000000000000227 ) ;
#19806=AXIS2_PLACEMENT_3D ( 'NONE', #613, #4316, #27059 ) ;
#19807=EDGE_CURVE ( 'NONE', #880, #24356, #19514, .T. ) ;
#19818=ORIENTED_EDGE ( 'NONE', *, *, #22902, .T. ) ;
#19827=CARTESIAN_POINT ( 'NONE',  ( -4.203833317240879275, -1.627343821129593859, -3.597273115243890818 ) ) ;
#19834=CARTESIAN_POINT ( 'NONE',  ( -1.274258131565027874, -3.883108878240886241, -3.220599429844051009 ) ) ;
#19839=CARTESIAN_POINT ( 'NONE',  ( 3.999999999999999112, 2.309401076758497595, -3.504271511726784194 ) ) ;
#19858=FACE_OUTER_BOUND ( 'NONE', #34814, .T. ) ;
#19962=CARTESIAN_POINT ( 'NONE',  ( -4.000000000000000000, 2.309401076758498483, -0.4999999999999927280 ) ) ;
#20125=CARTESIAN_POINT ( 'NONE',  ( 5.384454397937118664, 0.000000000000000000, -4.484454397937119197 ) ) ;
#20126=FACE_OUTER_BOUND ( 'NONE', #26920, .T. ) ;
#20192=CARTESIAN_POINT ( 'NONE',  ( -3.333333333333332149, -2.694301256218264218, -3.300726591567082036 ) ) ;
#20305=VERTEX_POINT ( 'NONE', #140 ) ;
#20379=CARTESIAN_POINT ( 'NONE',  ( 1.734723475976807094E-15, 4.618802153517012954, -0.4999999999999995559 ) ) ;
#20391=VECTOR ( 'NONE', #41929, 1000.000000000000114 ) ;
#20398=CARTESIAN_POINT ( 'NONE',  ( -2.000000000000002665, -3.464101615137770374, -3.142992957459237680 ) ) ;
#20423=CARTESIAN_POINT ( 'NONE',  ( 4.211140560182196957, 2.431303136016536470, -3.745885042887433514 ) ) ;
#20444=EDGE_CURVE ( 'NONE', #17801, #4036, #27509, .T. ) ;
#20446=PRODUCT_DEFINITION ( 'UNKNOWN', '', #26098, #22503 ) ;
#20486=PLANE ( 'NONE',  #26848 ) ;
#20491=CARTESIAN_POINT ( 'NONE',  ( 4.000000000000000000, -2.309401076758516691, -0.4999999999999995559 ) ) ;
#20499=CARTESIAN_POINT ( 'NONE',  ( 0.000000000000000000, 0.000000000000000000, -4.694516984716113228 ) ) ;
#20564=DIRECTION ( 'NONE',  ( -0.8660254037844373753, 0.5000000000000021094, 0.000000000000000000 ) ) ;
#20611=ADVANCED_FACE ( 'NONE', ( #15455 ), #14803, .F. ) ;
#20640=CARTESIAN_POINT ( 'NONE',  ( 3.510273485745307731, 2.827716139362654424, -3.610536846335885564 ) ) ;
#20680=VERTEX_POINT ( 'NONE', #41598 ) ;
#20715=ADVANCED_FACE ( 'NONE', ( #36532 ), #4817, .F. ) ;
#20741=CARTESIAN_POINT ( 'NONE',  ( 4.000000000000000000, 2.309401076758515803, -0.4999999999999995559 ) ) ;
#20822=AXIS2_PLACEMENT_3D ( 'NONE', #3470, #10474, #39687 ) ;
#20823=ADVANCED_FACE ( 'NONE', ( #26112 ), #37175, .F. ) ;
#20830=CARTESIAN_POINT ( 'NONE',  ( 0.6448876103708359731, 4.246476118072354922, -0.2256878752776725616 ) ) ;
#20844=CARTESIAN_POINT ( 'NONE',  ( -4.000000000000000000, 0.8730739991738342143, -3.223134629628428893 ) ) ;
#20857=CARTESIAN_POINT ( 'NONE',  ( -5.384454397937118664, 6.702023979852544604E-16, -5.000000000000000000 ) ) ;
#20870=CARTESIAN_POINT ( 'NONE',  ( 3.861362476283255685, 2.629030857715988656, -3.671615880910370500 ) ) ;
#20890=CARTESIAN_POINT ( 'NONE',  ( 4.000000000000000888, -0.8578082829538523635, -3.433262215449808696 ) ) ;
#20932=DIRECTION ( 'NONE',  ( -0.5000000000000016653, 0.8660254037844378194, 0.000000000000000000 ) ) ;
#20936=EDGE_LOOP ( 'NONE', ( #34356, #26376, #38163, #984 ) ) ;
#20990=B_SPLINE_CURVE_WITH_KNOTS ( 'NONE', 3,
 ( #6469, #19827, #13921, #16555 ),
 .UNSPECIFIED., .F., .F.,
 ( 4, 4 ),
 ( 0.000000000000000000, 0.002452478801916376308 ),
 .UNSPECIFIED. ) ;
#20994=FACE_OUTER_BOUND ( 'NONE', #1518, .T. ) ;
#21010=DIRECTION ( 'NONE',  ( 0.000000000000000000, 0.000000000000000000, -1.000000000000000000 ) ) ;
#21033=DIRECTION ( 'NONE',  ( 0.000000000000000000, 0.000000000000000000, -1.000000000000000000 ) ) ;
#21063=ORIENTED_EDGE ( 'NONE', *, *, #2560, .F. ) ;
#21102=CARTESIAN_POINT ( 'NONE',  ( 4.000000000000000000, 1.680228229147133767, -3.316631783032546021 ) ) ;
#21129=ORIENTED_EDGE ( 'NONE', *, *, #6053, .F. ) ;
#21247=DIRECTION ( 'NONE',  ( 1.000000000000000000, 0.000000000000000000, 0.000000000000000000 ) ) ;
#21311=CARTESIAN_POINT ( 'NONE',  ( -4.211140560182196957, 2.431303136016537803, -3.745885042887433514 ) ) ;
#21316=ORIENTED_EDGE ( 'NONE', *, *, #19807, .F. ) ;
#21393=FACE_OUTER_BOUND ( 'NONE', #7238, .T. ) ;
#21398=CARTESIAN_POINT ( 'NONE',  ( 4.141042297810615835, -2.227970268150433863, -3.687027686973623819 ) ) ;
#21432=ADVANCED_FACE ( 'NONE', ( #24727 ), #38009, .T. ) ;
#21456=CIRCLE ( 'NONE', #14478, 2.100000000000000089 ) ;
#21497=CARTESIAN_POINT ( 'NONE',  ( -4.000000000000000000, 1.700094919196744270, -3.320312364301766017 ) ) ;
#21527=DIRECTION ( 'NONE',  ( -0.000000000000000000, -0.000000000000000000, 1.000000000000000000 ) ) ;
#21658=B_SPLINE_CURVE_WITH_KNOTS ( 'NONE', 3,
 ( #36139, #19183, #39622, #19601, #22666, #26355 ),
 .UNSPECIFIED., .F., .F.,
 ( 4, 2, 4 ),
 ( -3.640115492409406142E-06, 0.0002066546034006526487, 0.0004169493222937146744 ),
 .UNSPECIFIED. ) ;
#21707=CARTESIAN_POINT ( 'NONE',  ( -5.384454397937118664, 6.594054843588581554E-16, -4.484454397937119197 ) ) ;
#21822=ORIENTED_EDGE ( 'NONE', *, *, #29509, .T. ) ;
#21827=DIRECTION ( 'NONE',  ( -1.000000000000000000, 0.000000000000000000, 0.000000000000000000 ) ) ;
#21915=DIRECTION ( 'NONE',  ( 1.224646799147353207E-16, 1.000000000000000000, 0.000000000000000000 ) ) ;
#22017=EDGE_LOOP ( 'NONE', ( #946, #35824, #34469, #21316 ) ) ;
#22027=CARTESIAN_POINT ( 'NONE',  ( 0.5469614295415388128, -4.303013824935362663, -3.535263753543555598 ) ) ;
#22092=AXIS2_PLACEMENT_3D ( 'NONE', #6859, #3563, #19775 ) ;
#22099=CIRCLE ( 'NONE', #39437, 2.100000000000000089 ) ;
#22163=CARTESIAN_POINT ( 'NONE',  ( -2.344047193898593395, -3.265465875126480455, -1.054683074273691752E-14 ) ) ;
#22165=ORIENTED_EDGE ( 'NONE', *, *, #30016, .F. ) ;
#22166=DIRECTION ( 'NONE',  ( 0.8660254037844379305, 0.5000000000000013323, 0.000000000000000000 ) ) ;
#22254=FACE_OUTER_BOUND ( 'NONE', #31120, .T. ) ;
#22276=CARTESIAN_POINT ( 'NONE',  ( 4.211140560182196957, 2.431303136016536470, -3.745885042887433514 ) ) ;
#22281=ORIENTED_EDGE ( 'NONE', *, *, #39936, .T. ) ;
#22346=B_SPLINE_CURVE_WITH_KNOTS ( 'NONE', 3,
 ( #40118, #17702, #30334, #17486, #3894, #23600, #30767, #40549 ),
 .UNSPECIFIED., .F., .F.,
 ( 4, 2, 2, 4 ),
 ( 0.000000000000000000, 0.002450665683189818828, 0.003675998524784728459, 0.004901331366379638524 ),
 .UNSPECIFIED. ) ;
#22362=B_SPLINE_CURVE_WITH_KNOTS ( 'NONE', 3,
 ( #24262, #37942, #1070, #11354, #17287, #34683 ),
 .UNSPECIFIED., .F., .F.,
 ( 4, 2, 4 ),
 ( 0.003358874760055550156, 0.004541967308452096383, 0.005725059856848641743 ),
 .UNSPECIFIED. ) ;
#22499=CARTESIAN_POINT ( 'NONE',  ( 0.000000000000000000, 0.000000000000000000, -4.484454397937119197 ) ) ;
#22503=PRODUCT_DEFINITION_CONTEXT ( 'detailed design', #40910, 'design' ) ;
#22510=CARTESIAN_POINT ( 'NONE',  ( 4.197393957002303999, 7.772902908466098641E-14, -3.503767560748929810 ) ) ;
#22546=CARTESIAN_POINT ( 'NONE',  ( -4.203934362469166963, -1.640673743454851286, -3.598432614606932756 ) ) ;
#22601=COLOUR_RGB ( '', 0.31764706, 0.68627451, 0.89019608) ;
#22659=CARTESIAN_POINT ( 'NONE',  ( -4.211140560182196957, 2.431303136016537803, -3.745885042887433514 ) ) ;
#22660=CARTESIAN_POINT ( 'NONE',  ( -6.259644161404860030E-16, -4.618802153517027165, -3.433295621305388234 ) ) ;
#22666=CARTESIAN_POINT ( 'NONE',  ( -4.000000000000000888, -2.309401076758512694, -3.504269196027526512 ) ) ;
#22707=VERTEX_POINT ( 'NONE', #2924 ) ;
#22723=DIRECTION ( 'NONE',  ( 0.000000000000000000, -0.000000000000000000, 1.000000000000000000 ) ) ;
#22739=ORIENTED_EDGE ( 'NONE', *, *, #16943, .T. ) ;
#22759=DIRECTION ( 'NONE',  ( 1.000000000000000000, 0.000000000000000000, 0.000000000000000000 ) ) ;
#22773=PRESENTATION_STYLE_ASSIGNMENT (( #26449 ) ) ;
#22791=CARTESIAN_POINT ( 'NONE',  ( -3.679171394226034675, -2.494631558665844739, -0.3503314178412558211 ) ) ;
#22867=CARTESIAN_POINT ( 'NONE',  ( 4.000000000000000000, -2.471525695159793035, -3.686886880705770864 ) ) ;
#22902=EDGE_CURVE ( 'NONE', #24319, #30609, #28927, .T. ) ;
#22932=ORIENTED_EDGE ( 'NONE', *, *, #20444, .T. ) ;
#22940=CARTESIAN_POINT ( 'NONE',  ( 2.499999999999999556, 0.000000000000000000, 3.469446951953614189E-15 ) ) ;
#22998=DIRECTION ( 'NONE',  ( 0.000000000000000000, 0.000000000000000000, -1.000000000000000000 ) ) ;
#23012=ORIENTED_EDGE ( 'NONE', *, *, #8070, .F. ) ;
#23051=ORIENTED_EDGE ( 'NONE', *, *, #26695, .F. ) ;
#23092=CARTESIAN_POINT ( 'NONE',  ( -2.805705207896067144, 3.226868319750155312, -3.503898532754364581 ) ) ;
#23118=CARTESIAN_POINT ( 'NONE',  ( -0.6810597143197697489, -4.461075778259609770, -3.598441714920717516 ) ) ;
#23122=ORIENTED_EDGE ( 'NONE', *, *, #34406, .F. ) ;
#23169=PRODUCT_DEFINITION_SHAPE ( 'NONE', 'NONE',  #20446 ) ;
#23178=LINE ( 'NONE', #36425, #32599 ) ;
#23199=( NAMED_UNIT ( * ) SI_UNIT ( $, .STERADIAN. ) SOLID_ANGLE_UNIT ( ) );
#23288=ORIENTED_EDGE ( 'NONE', *, *, #10424, .T. ) ;
#23297=CARTESIAN_POINT ( 'NONE',  ( 0.6666666666666658525, -4.233901974057276085, -3.300726591567086476 ) ) ;
#23320=CARTESIAN_POINT ( 'NONE',  ( -0.5449313310646672903, -4.304185902836978883, -3.316620875263469159 ) ) ;
#23346=DIRECTION ( 'NONE',  ( -0.000000000000000000, -0.000000000000000000, 1.000000000000000000 ) ) ;
#23376=CARTESIAN_POINT ( 'NONE',  ( 4.000000000000000000, 0.9868501483902631932, -0.09357334158579604100 ) ) ;
#23408=FILL_AREA_STYLE_COLOUR ( '', #22601 ) ;
#23471=CARTESIAN_POINT ( 'NONE',  ( 1.287237434362044075, 3.875615274277557809, -3.430618716626812059 ) ) ;
#23490=CARTESIAN_POINT ( 'NONE',  ( 0.000000000000000000, 0.000000000000000000, -4.694516984716113228 ) ) ;
#23507=ORIENTED_EDGE ( 'NONE', *, *, #32876, .F. ) ;
#23550=CARTESIAN_POINT ( 'NONE',  ( 2.687328764639642653, -3.067272167851299969, -0.05923475698271395140 ) ) ;
#23600=CARTESIAN_POINT ( 'NONE',  ( -3.510273485745307287, -2.827716139362669967, -3.610536846335890004 ) ) ;
#23662=EDGE_LOOP ( 'NONE', ( #584, #32799, #42336, #22165, #25860 ) ) ;
#23713=CARTESIAN_POINT ( 'NONE',  ( 3.999999999999998224, 2.472263674411418588, -3.687027874309861897 ) ) ;
#23729=EDGE_LOOP ( 'NONE', ( #6223, #15406, #7696, #23122 ) ) ;
#23863=AXIS2_PLACEMENT_3D ( 'NONE', #24279, #18382, #31642 ) ;
#23929=CARTESIAN_POINT ( 'NONE',  ( 0.000000000000000000, 0.000000000000000000, -4.000000000000000000 ) ) ;
#23939=UNCERTAINTY_MEASURE_WITH_UNIT (LENGTH_MEASURE( 1.000000000000000082E-05 ), #36668, 'distance_accuracy_value', 'NONE');
#23942=EDGE_LOOP ( 'NONE', ( #5286, #33600, #8869, #9683, #14793 ) ) ;
#23954=B_SPLINE_CURVE_WITH_KNOTS ( 'NONE', 3,
 ( #14356, #36809, #30073, #34392, #17652, #40287 ),
 .UNSPECIFIED., .F., .F.,
 ( 4, 2, 4 ),
 ( -3.640115492410698714E-06, 0.0002066546034006521879, 0.0004169493222937151081 ),
 .UNSPECIFIED. ) ;
#23962=EDGE_CURVE ( 'NONE', #22707, #38985, #1741, .T. ) ;
#23978=CARTESIAN_POINT ( 'NONE',  ( -2.000000000000006661, 3.464101615137750834, 0.000000000000000000 ) ) ;
#23979=ORIENTED_EDGE ( 'NONE', *, *, #4676, .F. ) ;
#24007=CARTESIAN_POINT ( 'NONE',  ( -4.000000000000000000, -2.309401076758512694, -3.433295621305382461 ) ) ;
#24021=EDGE_LOOP ( 'NONE', ( #37010, #15200, #24648, #25317 ) ) ;
#24153=CARTESIAN_POINT ( 'NONE',  ( 4.211140560182196957, -2.431303136016555122, -3.745885042887436622 ) ) ;
#24166=CARTESIAN_POINT ( 'NONE',  ( 0.000000000000000000, 0.000000000000000000, 0.000000000000000000 ) ) ;
#24224=ORIENTED_EDGE ( 'NONE', *, *, #6083, .T. ) ;
#24262=CARTESIAN_POINT ( 'NONE',  ( -4.000000000000000000, -2.309401076758515803, -0.4999999999999995559 ) ) ;
#24274=B_SPLINE_CURVE_WITH_KNOTS ( 'NONE', 3,
 ( #30338, #3674, #36419, #30566, #23376, #37295, #10691, #30128 ),
 .UNSPECIFIED., .F., .F.,
 ( 4, 2, 2, 4 ),
 ( 0.005725059856848645212, 0.006314084072593634418, 0.006903108288338624492, 0.008081156719828603771 ),
 .UNSPECIFIED. ) ;
#24279=CARTESIAN_POINT ( 'NONE',  ( 0.000000000000000000, 0.000000000000000000, -4.974599999999998801 ) ) ;
#24319=VERTEX_POINT ( 'NONE', #22940 ) ;
#24335=B_SPLINE_CURVE_WITH_KNOTS ( 'NONE', 3,
 ( #28440, #18852, #32313, #8337, #12271 ),
 .UNSPECIFIED., .F., .F.,
 ( 4, 1, 4 ),
 ( 0.000000000000000000, 0.002309401076758505356, 0.004618802153517010713 ),
 .UNSPECIFIED. ) ;
#24351=AXIS2_PLACEMENT_3D ( 'NONE', #14310, #539, #37190 ) ;
#24356=VERTEX_POINT ( 'NONE', #16594 ) ;
#24429=B_SPLINE_CURVE_WITH_KNOTS ( 'NONE', 3,
 ( #36958, #7069, #31075, #41079, #17589, #20640, #20870, #20423 ),
 .UNSPECIFIED., .F., .F.,
 ( 4, 2, 2, 4 ),
 ( 7.780516681398759253E-20, 0.002450665683189819696, 0.003675998524784729327, 0.004901331366379639391 ),
 .UNSPECIFIED. ) ;
#24448=CARTESIAN_POINT ( 'NONE',  ( -4.000000000000000888, -1.539600717839011201, -3.300726591567081591 ) ) ;
#24489=ORIENTED_EDGE ( 'NONE', *, *, #17311, .F. ) ;
#24510=ORIENTED_EDGE ( 'NONE', *, *, #6370, .F. ) ;
#24545=AXIS2_PLACEMENT_3D ( 'NONE', #42614, #19752, #26496 ) ;
#24648=ORIENTED_EDGE ( 'NONE', *, *, #8211, .F. ) ;
#24650=CARTESIAN_POINT ( 'NONE',  ( 3.522875095019493141, -2.820352903225631369, -3.598441714920572299 ) ) ;
#24653=CONICAL_SURFACE ( 'NONE', #14894, 4.000000000000000000, 0.8911886515913786111 ) ;
#24669=VERTEX_POINT ( 'NONE', #30607 ) ;
#24692=VECTOR ( 'NONE', #32189, 1000.000000000000227 ) ;
#24708=PRODUCT_CONTEXT ( 'NONE', #3559, 'mechanical' ) ;
#24727=FACE_OUTER_BOUND ( 'NONE', #28094, .T. ) ;
#24814=ORIENTED_EDGE ( 'NONE', *, *, #39936, .F. ) ;
#24851=ORIENTED_EDGE ( 'NONE', *, *, #41388, .F. ) ;
#24876=ADVANCED_FACE ( 'NONE', ( #26868 ), #13803, .T. ) ;
#24879=CARTESIAN_POINT ( 'NONE',  ( 0.000000000000000000, 0.000000000000000000, -25.03750572909317285 ) ) ;
#24884=CARTESIAN_POINT ( 'NONE',  ( 0.5276280594147412240, -4.314175951381924889, -3.320322319201654881 ) ) ;
#24891=( BOUNDED_SURFACE ( )  B_SPLINE_SURFACE ( 3, 2, ( 
 ( #15041, #1265, #34861 ),
 ( #24884, #22027, #34646 ),
 ( #4976, #18547, #37694 ),
 ( #5407, #41387, #28351 ),
 ( #38343, #11321, #24650 ),
 ( #37906, #21398, #18775 ) ),
 .UNSPECIFIED., .F., .F., .F. ) 
 B_SPLINE_SURFACE_WITH_KNOTS ( ( 4, 2, 4 ),
 ( 3, 3 ),
 ( 0.02032853247518126918, 0.02278863295364821906, 0.02524873343211517240 ),
 ( 0.000000000000000000, 1.000000000000000000 ),
 .UNSPECIFIED. ) 
 GEOMETRIC_REPRESENTATION_ITEM ( )  RATIONAL_B_SPLINE_SURFACE ( (
 ( 1.000000000000000000, 0.8047781615896837382, 1.000000000000000000),
 ( 1.000000000000000000, 0.8123767586289252218, 1.000000000000000000),
 ( 1.000000000000000000, 0.8190662415564388121, 1.000000000000000000),
 ( 1.000000000000000000, 0.8192361015669026303, 1.000000000000000000),
 ( 1.000000000000000000, 0.8126135807103900266, 1.000000000000000000),
 ( 1.000000000000000000, 0.8047712338318593339, 1.000000000000000000) ) ) 
 REPRESENTATION_ITEM ( '' )  SURFACE ( )  );
#24967=CARTESIAN_POINT ( 'NONE',  ( -2.725741868435985094, 3.045094352034055429, -3.220599429844047012 ) ) ;
#24982=ORIENTED_EDGE ( 'NONE', *, *, #17492, .F. ) ;
#25071=CARTESIAN_POINT ( 'NONE',  ( 3.679171394226031122, 2.494631558665830973, -0.3503314178412474389 ) ) ;
#25095=CARTESIAN_POINT ( 'NONE',  ( 2.500000000000000888, 3.061616997868384127E-16, -4.974599999999998801 ) ) ;
#25098=FACE_OUTER_BOUND ( 'NONE', #1255, .T. ) ;
#25101=DIRECTION ( 'NONE',  ( 0.000000000000000000, 0.000000000000000000, -1.000000000000000000 ) ) ;
#25170=ORIENTED_EDGE ( 'NONE', *, *, #27134, .T. ) ;
#25172=CARTESIAN_POINT ( 'NONE',  ( -0.6640947660597427138, 4.471078309994878985, -3.602146406945963442 ) ) ;
#25195=CARTESIAN_POINT ( 'NONE',  ( -2.500000000000000888, 0.000000000000000000, -4.974599999999998801 ) ) ;
#25224=CARTESIAN_POINT ( 'NONE',  ( 0.000000000000000000, 0.000000000000000000, 0.000000000000000000 ) ) ;
#25298=DIRECTION ( 'NONE',  ( -0.000000000000000000, -0.000000000000000000, 1.000000000000000000 ) ) ;
#25317=ORIENTED_EDGE ( 'NONE', *, *, #1184, .F. ) ;
#25325=CARTESIAN_POINT ( 'NONE',  ( 0.6507732100473444525, -4.243078065514795050, -0.2236248678334952777 ) ) ;
#25354=B_SPLINE_CURVE_WITH_KNOTS ( 'NONE', 3,
 ( #22659, #9741, #23092, #35906, #19593, #42246, #32440, #25723 ),
 .UNSPECIFIED., .F., .F.,
 ( 4, 2, 2, 4 ),
 ( 0.000000000000000000, 0.002450665683189820997, 0.003675998524784731495, 0.004901331366379641993 ),
 .UNSPECIFIED. ) ;
#25355=SHAPE_DEFINITION_REPRESENTATION ( #23169, #37437 ) ;
#25452=EDGE_LOOP ( 'NONE', ( #23051, #41325, #12638, #9327 ) ) ;
#25462=VERTEX_POINT ( 'NONE', #43162 ) ;
#25474=VERTEX_POINT ( 'NONE', #20741 ) ;
#25497=CARTESIAN_POINT ( 'NONE',  ( -3.355112389629170799, 2.681727112203152963, -0.2256878752776689534 ) ) ;
#25519=STYLED_ITEM ( 'NONE', ( #26836 ), #28157 ) ;
#25601=AXIS2_PLACEMENT_3D ( 'NONE', #40644, #21527, #4219 ) ;
#25674=EDGE_LOOP ( 'NONE', ( #261, #12499, #25823 ) ) ;
#25723=CARTESIAN_POINT ( 'NONE',  ( 1.411581201560190495E-15, 4.862606272033091592, -3.745885042887436622 ) ) ;
#25823=ORIENTED_EDGE ( 'NONE', *, *, #14774, .F. ) ;
#25860=ORIENTED_EDGE ( 'NONE', *, *, #27134, .F. ) ;
#25979=DIRECTION ( 'NONE',  ( 0.000000000000000000, 0.000000000000000000, -1.000000000000000000 ) ) ;
#26012=ADVANCED_FACE ( 'NONE', ( #27643 ), #24653, .T. ) ;
#26098=PRODUCT_DEFINITION_FORMATION_WITH_SPECIFIED_SOURCE ( 'ANY', '', #26283, .NOT_KNOWN. ) ;
#26112=FACE_OUTER_BOUND ( 'NONE', #33223, .T. ) ;
#26150=CARTESIAN_POINT ( 'NONE',  ( -2.742827927723112236, -3.035229711105190464, -3.433252694550595230 ) ) ;
#26186=DIRECTION ( 'NONE',  ( -1.000000000000000000, 0.000000000000000000, 0.000000000000000000 ) ) ;
#26190=ORIENTED_EDGE ( 'NONE', *, *, #19807, .T. ) ;
#26227=EDGE_CURVE ( 'NONE', #6210, #40010, #42622, .T. ) ;
#26281=ORIENTED_EDGE ( 'NONE', *, *, #39576, .F. ) ;
#26283=PRODUCT ( 'hex flange nut gradea_iso_ISO - 4161 - M5 - N', 'hex flange nut gradea_iso_ISO - 4161 - M5 - N', '', ( #24708 ) ) ;
#26355=CARTESIAN_POINT ( 'NONE',  ( -4.000000000000000000, -2.309401076758512694, -3.433295621305382461 ) ) ;
#26376=ORIENTED_EDGE ( 'NONE', *, *, #9438, .T. ) ;
#26398=CARTESIAN_POINT ( 'NONE',  ( 4.000000000000000888, 1.539600717838996990, -3.300726591567079815 ) ) ;
#26449=SURFACE_STYLE_USAGE ( .BOTH. , #42999 ) ;
#26496=DIRECTION ( 'NONE',  ( -1.000000000000000000, 0.000000000000000000, 0.000000000000000000 ) ) ;
#26554=AXIS2_PLACEMENT_3D ( 'NONE', #12549, #5558, #18916 ) ;
#26591=VERTEX_POINT ( 'NONE', #35350 ) ;
#26603=DIRECTION ( 'NONE',  ( 1.000000000000000000, 0.000000000000000000, 0.000000000000000000 ) ) ;
#26604=CARTESIAN_POINT ( 'NONE',  ( -2.100000000000000089, 2.571758278209441957E-16, -5.000000000000000000 ) ) ;
#26616=PLANE ( 'NONE',  #17037 ) ;
#26646=AXIS2_PLACEMENT_3D ( 'NONE', #34286, #27546, #11188 ) ;
#26663=SHAPE_REPRESENTATION_RELATIONSHIP ( 'NONE' , 'NONE' ,  #37437, #35926 ) ;
#26676=ADVANCED_FACE ( 'NONE', ( #29462, #29044 ), #26616, .T. ) ;
#26687=CARTESIAN_POINT ( 'NONE',  ( 1.312671235360372224, 3.860931062424219462, -0.05923475698270440348 ) ) ;
#26695=EDGE_CURVE ( 'NONE', #20680, #24669, #8623, .T. ) ;
#26699=EDGE_CURVE ( 'NONE', #14639, #11201, #18772, .T. ) ;
#26717=CARTESIAN_POINT ( 'NONE',  ( 2.500000000000000444, 0.000000000000000000, -25.03750572909317285 ) ) ;
#26784=CARTESIAN_POINT ( 'NONE',  ( -2.836893136758495970, -3.208949435745868328, -3.505054077164885484 ) ) ;
#26798=ORIENTED_EDGE ( 'NONE', *, *, #40319, .T. ) ;
#26835=EDGE_CURVE ( 'NONE', #29982, #25462, #30249, .T. ) ;
#26836=PRESENTATION_STYLE_ASSIGNMENT (( #32572 ) ) ;
#26848=AXIS2_PLACEMENT_3D ( 'NONE', #33749, #20932, #128 ) ;
#26868=FACE_OUTER_BOUND ( 'NONE', #8949, .T. ) ;
#26878=AXIS2_PLACEMENT_3D ( 'NONE', #1521, #21010, #41010 ) ;
#26920=EDGE_LOOP ( 'NONE', ( #42300, #10760, #17476 ) ) ;
#26944=AXIS2_PLACEMENT_3D ( 'NONE', #10732, #21033, #886 ) ;
#26953=EDGE_LOOP ( 'NONE', ( #30029, #992, #1776 ) ) ;
#26984=UNCERTAINTY_MEASURE_WITH_UNIT (LENGTH_MEASURE( 1.000000000000000082E-05 ), #211, 'distance_accuracy_value', 'NONE');
#27004=ORIENTED_EDGE ( 'NONE', *, *, #39889, .F. ) ;
#27042=CARTESIAN_POINT ( 'NONE',  ( 5.384454397937118664, 0.000000000000000000, -5.000000000000000000 ) ) ;
#27048=EDGE_CURVE ( 'NONE', #31862, #959, #15486, .T. ) ;
#27059=DIRECTION ( 'NONE',  ( -1.000000000000000000, 0.000000000000000000, 0.000000000000000000 ) ) ;
#27074=CARTESIAN_POINT ( 'NONE',  ( 0.000000000000000000, 0.000000000000000000, 0.000000000000000000 ) ) ;
#27134=EDGE_CURVE ( 'NONE', #37442, #29982, #34311, .T. ) ;
#27146=LINE ( 'NONE', #29771, #11937 ) ;
#27371=CARTESIAN_POINT ( 'NONE',  ( 3.472371940585993855, 2.614027278893175321, -3.320322319201766792 ) ) ;
#27380=CARTESIAN_POINT ( 'NONE',  ( -2.500000000000000444, 3.061616997868383634E-16, -25.03750572909317285 ) ) ;
#27395=CARTESIAN_POINT ( 'NONE',  ( 4.000000000000000000, 0.8378280264232961239, -3.220590601395640018 ) ) ;
#27434=CARTESIAN_POINT ( 'NONE',  ( 4.000000000000000000, -2.309401076758514915, -3.433295621305383349 ) ) ;
#27442=CARTESIAN_POINT ( 'NONE',  ( 0.000000000000000000, 0.000000000000000000, 0.000000000000000000 ) ) ;
#27456=ORIENTED_EDGE ( 'NONE', *, *, #32299, .F. ) ;
#27509=B_SPLINE_CURVE_WITH_KNOTS ( 'NONE', 3,
 ( #23978, #14590, #10430, #17661, #37244, #34623 ),
 .UNSPECIFIED., .F., .F.,
 ( 4, 2, 4 ),
 ( 0.002365888236227977302, 0.003551327329835078910, 0.004736766423442180518 ),
 .UNSPECIFIED. ) ;
#27546=DIRECTION ( 'NONE',  ( 0.000000000000000000, 0.000000000000000000, -1.000000000000000000 ) ) ;
#27564=VERTEX_POINT ( 'NONE', #989 ) ;
#27620=CARTESIAN_POINT ( 'NONE',  ( 4.000000000000000000, 2.512223110932545023, -3.469391141908803711 ) ) ;
#27634=CARTESIAN_POINT ( 'NONE',  ( 4.000000000000000000, 2.309401076758497151, -5.000000000000000000 ) ) ;
#27643=FACE_OUTER_BOUND ( 'NONE', #10086, .T. ) ;
#27677=ORIENTED_EDGE ( 'NONE', *, *, #1218, .F. ) ;
#27779=DIRECTION ( 'NONE',  ( -0.000000000000000000, -0.000000000000000000, 1.000000000000000000 ) ) ;
#27785=CARTESIAN_POINT ( 'NONE',  ( -2.712762565639006418, 3.052587955997511759, -3.430618716626627318 ) ) ;
#27811=DIRECTION ( 'NONE',  ( -0.000000000000000000, 0.000000000000000000, -1.000000000000000000 ) ) ;
#27976=CIRCLE ( 'NONE', #15435, 5.384454397937118664 ) ;
#27977=ORIENTED_EDGE ( 'NONE', *, *, #34482, .T. ) ;
#28015=CARTESIAN_POINT ( 'NONE',  ( -4.197393957002303999, -7.773935952363655451E-14, -3.503767560748929810 ) ) ;
#28029=CARTESIAN_POINT ( 'NONE',  ( 2.100000000000000089, 0.000000000000000000, -5.000000000000000000 ) ) ;
#28070=AXIS2_PLACEMENT_3D ( 'NONE', #20499, #40070, #14159 ) ;
#28080=ORIENTED_EDGE ( 'NONE', *, *, #42423, .T. ) ;
#28094=EDGE_LOOP ( 'NONE', ( #27004, #1914, #26190, #13807 ) ) ;
#28157=MANIFOLD_SOLID_BREP ( 'EndChamfer', #6570 ) ;
#28161=STYLED_ITEM ( 'NONE', ( #22773 ), #35926 ) ;
#28223=CARTESIAN_POINT ( 'NONE',  ( -4.197477534772231955, 0.8522413273724368521, -3.505042416683225692 ) ) ;
#28351=CARTESIAN_POINT ( 'NONE',  ( 2.807080416178989513, -3.225969019225150003, -3.502507215260505014 ) ) ;
#28362=CARTESIAN_POINT ( 'NONE',  ( 2.500000000000000888, 3.061616997868384127E-16, -4.974599999999998801 ) ) ;
#28440=CARTESIAN_POINT ( 'NONE',  ( 4.000000000000000000, 2.309401076758497151, -3.433295621305379353 ) ) ;
#28448=CARTESIAN_POINT ( 'NONE',  ( -4.000000000000000000, -0.8232339106130515116, -3.430630286862743183 ) ) ;
#28522=CARTESIAN_POINT ( 'NONE',  ( 5.560781378645573980, 6.809993116116507654E-16, -4.000000000000000000 ) ) ;
#28562=LINE ( 'NONE', #8253, #1211 ) ;
#28588=ADVANCED_FACE ( 'NONE', ( #14844 ), #34642, .F. ) ;
#28683=CARTESIAN_POINT ( 'NONE',  ( -4.000000000000000000, -2.309401076758515803, -0.4999999999999995559 ) ) ;
#28739=CARTESIAN_POINT ( 'NONE',  ( 4.000000000000000000, 2.309401076758515803, -0.4999999999999995559 ) ) ;
#28771=DIRECTION ( 'NONE',  ( 0.000000000000000000, -0.000000000000000000, 1.000000000000000000 ) ) ;
#28927=CIRCLE ( 'NONE', #10080, 2.499999999999999556 ) ;
#28956=VERTEX_POINT ( 'NONE', #42437 ) ;
#28962=CARTESIAN_POINT ( 'NONE',  ( -6.473970235329672780E-16, -4.862606272033106691, -3.745885042887442395 ) ) ;
#28978=CARTESIAN_POINT ( 'NONE',  ( -1.144235203016679359, -3.958177651039096911, -0.09382832055446428676 ) ) ;
#29021=AXIS2_PLACEMENT_3D ( 'NONE', #30791, #1085, #20564 ) ;
#29044=FACE_OUTER_BOUND ( 'NONE', #42545, .T. ) ;
#29105=EDGE_CURVE ( 'NONE', #7662, #31862, #21456, .T. ) ;
#29146=VERTEX_POINT ( 'NONE', #11032 ) ;
#29196=CARTESIAN_POINT ( 'NONE',  ( -2.688821387764050996E-14, -4.618802153517012954, -0.4999999999999995559 ) ) ;
#29203=CARTESIAN_POINT ( 'NONE',  ( -1.999999999999999556, 3.464101615137754830, -3.142992957459232795 ) ) ;
#29213=CARTESIAN_POINT ( 'NONE',  ( -1.390230914382372118, -4.043987460488664532, -3.502507215260523665 ) ) ;
#29265=DIRECTION ( 'NONE',  ( 0.000000000000000000, 0.000000000000000000, 1.000000000000000000 ) ) ;
#29273=EDGE_CURVE ( 'NONE', #17801, #27564, #4666, .T. ) ;
#29305=VERTEX_POINT ( 'NONE', #4894 ) ;
#29335=EDGE_LOOP ( 'NONE', ( #21063, #10003, #32266, #29582 ) ) ;
#29462=FACE_BOUND ( 'NONE', #40430, .T. ) ;
#29509=EDGE_CURVE ( 'NONE', #30609, #24319, #38149, .T. ) ;
#29570=VECTOR ( 'NONE', #31831, 1000.000000000000114 ) ;
#29582=ORIENTED_EDGE ( 'NONE', *, *, #10424, .F. ) ;
#29597=CARTESIAN_POINT ( 'NONE',  ( -1.240299975428113101E-15, -4.647091401871173311, -3.572172305156514849 ) ) ;
#29623=CIRCLE ( 'NONE', #10808, 2.500000000000000888 ) ;
#29644=CARTESIAN_POINT ( 'NONE',  ( 4.197393957002303999, 0.8151795401431359833, -3.503767560748935139 ) ) ;
#29726=( NAMED_UNIT ( * ) PLANE_ANGLE_UNIT ( ) SI_UNIT ( $, .RADIAN. ) );
#29729=EDGE_CURVE ( 'NONE', #4036, #27564, #37738, .T. ) ;
#29771=CARTESIAN_POINT ( 'NONE',  ( -4.000000000000000000, 2.309401076758498483, -5.000000000000000000 ) ) ;
#29772=ADVANCED_FACE ( 'NONE', ( #7893 ), #16587, .F. ) ;
#29803=ORIENTED_EDGE ( 'NONE', *, *, #10997, .T. ) ;
#29822=DIRECTION ( 'NONE',  ( 1.000000000000000000, 0.000000000000000000, 0.000000000000000000 ) ) ;
#29869=CARTESIAN_POINT ( 'NONE',  ( -2.756197834950067094, -3.027510591568735254, -3.223146290109809797 ) ) ;
#29877=CARTESIAN_POINT ( 'NONE',  ( 3.355112389629172576, -2.681727112203168950, -0.2256878752776777242 ) ) ;
#29914=FILL_AREA_STYLE ('',( #12525 ) ) ;
#29917=ORIENTED_EDGE ( 'NONE', *, *, #26835, .T. ) ;
#29951=FACE_OUTER_BOUND ( 'NONE', #39826, .T. ) ;
#29982=VERTEX_POINT ( 'NONE', #35372 ) ;
#30016=EDGE_CURVE ( 'NONE', #29982, #25474, #24274, .T. ) ;
#30029=ORIENTED_EDGE ( 'NONE', *, *, #1960, .T. ) ;
#30039=DIRECTION ( 'NONE',  ( -0.000000000000000000, -0.000000000000000000, 1.000000000000000000 ) ) ;
#30073=CARTESIAN_POINT ( 'NONE',  ( -4.101948962585906244, 2.368261337751074169, -3.681124513963621503 ) ) ;
#30113=EDGE_CURVE ( 'NONE', #14112, #17801, #18748, .T. ) ;
#30128=CARTESIAN_POINT ( 'NONE',  ( 4.000000000000000000, 2.309401076758515803, -0.4999999999999995559 ) ) ;
#30137=ADVANCED_FACE ( 'NONE', ( #20126 ), #11745, .T. ) ;
#30167=ORIENTED_EDGE ( 'NONE', *, *, #7583, .T. ) ;
#30249=CIRCLE ( 'NONE', #19806, 4.000000000000000000 ) ;
#30274=TOROIDAL_SURFACE ( 'NONE', #39296, 5.384454397937118664, 0.5155456020628804703 ) ;
#30304=DIRECTION ( 'NONE',  ( 0.000000000000000000, 0.000000000000000000, 1.000000000000000000 ) ) ;
#30334=CARTESIAN_POINT ( 'NONE',  ( -1.391697335622809950, -4.043246145443391448, -3.503898532754372575 ) ) ;
#30338=CARTESIAN_POINT ( 'NONE',  ( 4.000000000000000000, 0.000000000000000000, 0.000000000000000000 ) ) ;
#30392=CARTESIAN_POINT ( 'NONE',  ( 1.654252653721905331, 3.663718938583014229, -0.01223254789873410957 ) ) ;
#30414=ORIENTED_EDGE ( 'NONE', *, *, #29729, .T. ) ;
#30566=CARTESIAN_POINT ( 'NONE',  ( 4.000000000000000000, 0.7924765000094659007, -0.05906175389889852662 ) ) ;
#30607=CARTESIAN_POINT ( 'NONE',  ( 2.500000000000000444, 0.000000000000000000, -5.000000000000000888 ) ) ;
#30609=VERTEX_POINT ( 'NONE', #33494 ) ;
#30663=CARTESIAN_POINT ( 'NONE',  ( 0.000000000000000000, 0.000000000000000000, 3.469446951953614189E-15 ) ) ;
#30719=DIRECTION ( 'NONE',  ( -0.000000000000000000, -0.000000000000000000, 1.000000000000000000 ) ) ;
#30733=PLANE ( 'NONE',  #11596 ) ;
#30760=B_SPLINE_CURVE_WITH_KNOTS ( 'NONE', 3,
 ( #39002, #19839, #32894, #36370, #2970, #19623 ),
 .UNSPECIFIED., .F., .F.,
 ( 4, 2, 4 ),
 ( 0.000000000000000000, 0.0002095117440854730670, 0.0004190234881709461339 ),
 .UNSPECIFIED. ) ;
#30767=CARTESIAN_POINT ( 'NONE',  ( -3.861362476283256129, -2.629030857716004199, -3.671615880910374941 ) ) ;
#30791=CARTESIAN_POINT ( 'NONE',  ( 4.000000000000000000, 2.309401076758497151, -5.000000000000000000 ) ) ;
#30955=CARTESIAN_POINT ( 'NONE',  ( -4.000000000000000000, -7.806255641895631925E-15, -3.142992957459232350 ) ) ;
#31033=CARTESIAN_POINT ( 'NONE',  ( 0.1750025118121568690, 4.719839900820621104, -3.469254087858248070 ) ) ;
#31075=CARTESIAN_POINT ( 'NONE',  ( 1.391697335622810172, 4.043246145443375461, -3.503898532754365913 ) ) ;
#31076=FACE_OUTER_BOUND ( 'NONE', #25452, .T. ) ;
#31104=CARTESIAN_POINT ( 'NONE',  ( -4.000000000000000888, 1.563622288139195238, -0.2253451193528307472 ) ) ;
#31120=EDGE_LOOP ( 'NONE', ( #14911, #2787, #18534, #2022, #34951, #13056 ) ) ;
#31152=CARTESIAN_POINT ( 'NONE',  ( -3.974344831685191280E-13, 4.796734841935104576, -3.721909803043223608 ) ) ;
#31189=CARTESIAN_POINT ( 'NONE',  ( 4.000000000000000000, 0.000000000000000000, 0.000000000000000000 ) ) ;
#31271=FACE_OUTER_BOUND ( 'NONE', #40619, .T. ) ;
#31303=AXIS2_PLACEMENT_3D ( 'NONE', #38528, #8650, #38112 ) ;
#31311=DIRECTION ( 'NONE',  ( -0.000000000000000000, 0.000000000000000000, -1.000000000000000000 ) ) ;
#31418=CARTESIAN_POINT ( 'NONE',  ( -2.688821387764050996E-14, -4.618802153517012954, -0.4999999999999995559 ) ) ;
#31517=FACE_OUTER_BOUND ( 'NONE', #23942, .T. ) ;
#31524=DIRECTION ( 'NONE',  ( 1.000000000000000000, 0.000000000000000000, 0.000000000000000000 ) ) ;
#31536=CARTESIAN_POINT ( 'NONE',  ( -4.000000000000000000, 0.9868501483902560878, -0.09357334158579519445 ) ) ;
#31549=DIRECTION ( 'NONE',  ( -1.000000000000000000, 0.000000000000000000, 0.000000000000000000 ) ) ;
#31642=DIRECTION ( 'NONE',  ( 1.000000000000000000, 0.000000000000000000, 0.000000000000000000 ) ) ;
#31652=DIRECTION ( 'NONE',  ( 0.000000000000000000, 0.000000000000000000, 1.000000000000000000 ) ) ;
#31727=PLANE ( 'NONE',  #4730 ) ;
#31831=DIRECTION ( 'NONE',  ( 0.8191520442889902442, 1.003171929053522651E-16, -0.5735764363510482688 ) ) ;
#31848=CARTESIAN_POINT ( 'NONE',  ( 1.655952806101427033, -3.662737355149048302, -1.182683869819604841E-14 ) ) ;
#31862=VERTEX_POINT ( 'NONE', #32022 ) ;
#31892=CARTESIAN_POINT ( 'NONE',  ( 0.000000000000000000, 0.000000000000000000, -4.484454397937119197 ) ) ;
#31908=EDGE_CURVE ( 'NONE', #14639, #37442, #15030, .T. ) ;
#31920=CARTESIAN_POINT ( 'NONE',  ( 4.198928548860774157, -0.8158838809860124996, -3.526471437616918170 ) ) ;
#31948=CARTESIAN_POINT ( 'NONE',  ( -2.682243648011671588, -3.070208061305317759, -0.04852650426602272971 ) ) ;
#31962=ORIENTED_EDGE ( 'NONE', *, *, #42790, .T. ) ;
#31987=AXIS2_PLACEMENT_3D ( 'NONE', #36323, #36117, #29822 ) ;
#32022=CARTESIAN_POINT ( 'NONE',  ( 2.100000000000000089, 0.000000000000000000, -4.694516984716113228 ) ) ;
#32039=CARTESIAN_POINT ( 'NONE',  ( 4.000000000000000000, -1.942223658245635809, -0.3516579909967643691 ) ) ;
#32090=VECTOR ( 'NONE', #31652, 1000.000000000000000 ) ;
#32146=CARTESIAN_POINT ( 'NONE',  ( -2.000000000000006661, 3.464101615137750834, 0.000000000000000000 ) ) ;
#32147=( NAMED_UNIT ( * ) SI_UNIT ( $, .STERADIAN. ) SOLID_ANGLE_UNIT ( ) );
#32189=DIRECTION ( 'NONE',  ( 0.9396926207859138680, 1.150791560227856926E-16, -0.3420201433256536139 ) ) ;
#32232=CARTESIAN_POINT ( 'NONE',  ( -0.6448876103708541807, -4.246476118072358474, -0.2256878752776773356 ) ) ;
#32266=ORIENTED_EDGE ( 'NONE', *, *, #23962, .F. ) ;
#32299=EDGE_CURVE ( 'NONE', #35337, #959, #29623, .T. ) ;
#32313=CARTESIAN_POINT ( 'NONE',  ( 2.000000000000000444, 3.464101615137754830, -3.142992957459231018 ) ) ;
#32439=AXIS2_PLACEMENT_3D ( 'NONE', #27634, #4466, #11058 ) ;
#32440=CARTESIAN_POINT ( 'NONE',  ( -0.3461262719736137305, 4.658553426539289610, -3.671615880910373608 ) ) ;
#32465=CARTESIAN_POINT ( 'NONE',  ( 0.1410422978106145031, -4.700232962125109104, -3.687027686973628704 ) ) ;
#32473=VECTOR ( 'NONE', #30304, 1000.000000000000000 ) ;
#32572=SURFACE_STYLE_USAGE ( .BOTH. , #19298 ) ;
#32599=VECTOR ( 'NONE', #42544, 1000.000000000000000 ) ;
#32605=AXIS2_PLACEMENT_3D ( 'NONE', #27074, #3251, #6533 ) ;
#32648=ADVANCED_FACE ( 'NONE', ( #4142 ), #1758, .T. ) ;
#32799=ORIENTED_EDGE ( 'NONE', *, *, #32876, .T. ) ;
#32876=EDGE_CURVE ( 'NONE', #14639, #28956, #622, .T. ) ;
#32879=B_SPLINE_CURVE_WITH_KNOTS ( 'NONE', 3,
 ( #28015, #11212, #15151, #34961, #5288, #37796 ),
 .UNSPECIFIED., .F., .F.,
 ( 4, 2, 4 ),
 ( 0.002452478801916376308, 0.003676905084148007850, 0.004901331366379639391 ),
 .UNSPECIFIED. ) ;
#32894=CARTESIAN_POINT ( 'NONE',  ( 4.024499207728657879, 2.323545700935571556, -3.572172305156506411 ) ) ;
#32896=EDGE_CURVE ( 'NONE', #7662, #29305, #13313, .T. ) ;
#32980=MECHANICAL_DESIGN_GEOMETRIC_PRESENTATION_REPRESENTATION('',(#28161),#921);
#33126=DIRECTION ( 'NONE',  ( -0.5000000000000019984, -0.8660254037844375974, 0.000000000000000000 ) ) ;
#33198=CARTESIAN_POINT ( 'NONE',  ( 0.000000000000000000, 0.000000000000000000, 0.000000000000000000 ) ) ;
#33204=CARTESIAN_POINT ( 'NONE',  ( -2.000000000000007550, -3.464101615137749945, 0.000000000000000000 ) ) ;
#33223=EDGE_LOOP ( 'NONE', ( #42598, #24814, #18165, #39210, #23507 ) ) ;
#33225=CARTESIAN_POINT ( 'NONE',  ( 0.3198814748697593746, 4.434118497892183264, -0.3507732604232499107 ) ) ;
#33278=ORIENTED_EDGE ( 'NONE', *, *, #10348, .T. ) ;
#33306=DIRECTION ( 'NONE',  ( 1.000000000000000000, 0.000000000000000000, 0.000000000000000000 ) ) ;
#33405=EDGE_CURVE ( 'NONE', #22707, #14639, #17764, .T. ) ;
#33413=SURFACE_STYLE_FILL_AREA ( #3496 ) ;
#33478=CIRCLE ( 'NONE', #37647, 5.560781378645573980 ) ;
#33494=CARTESIAN_POINT ( 'NONE',  ( -2.499999999999999556, 3.061616997868382648E-16, 3.469446951953614189E-15 ) ) ;
#33588=ADVANCED_FACE ( 'NONE', ( #973 ), #14327, .F. ) ;
#33600=ORIENTED_EDGE ( 'NONE', *, *, #33405, .T. ) ;
#33644=CARTESIAN_POINT ( 'NONE',  ( 1.144235203016666258, 3.958177651039090250, -0.09382832055445661235 ) ) ;
#33657=CARTESIAN_POINT ( 'NONE',  ( -6.259644161404860030E-16, -4.618802153517027165, -3.433295621305388234 ) ) ;
#33666=CARTESIAN_POINT ( 'NONE',  ( -4.000000000000000000, 2.309401076758498483, -3.433295621305379353 ) ) ;
#33678=CARTESIAN_POINT ( 'NONE',  ( 2.756197834950227410, 3.027510591568626896, -3.223146290109805356 ) ) ;
#33749=CARTESIAN_POINT ( 'NONE',  ( 1.567478505476134606E-15, 4.618802153517012066, -5.000000000000000000 ) ) ;
#33758=CARTESIAN_POINT ( 'NONE',  ( 2.855764796983346177, -2.970025579236428737, -0.09382832055446485575 ) ) ;
#33820=ORIENTED_EDGE ( 'NONE', *, *, #14774, .T. ) ;
#33860=FACE_OUTER_BOUND ( 'NONE', #20936, .T. ) ;
#33962=VERTEX_POINT ( 'NONE', #33666 ) ;
#34054=EDGE_CURVE ( 'NONE', #29146, #4036, #39978, .T. ) ;
#34119=CARTESIAN_POINT ( 'NONE',  ( -0.1410422978106123659, 4.700232962125094893, -3.687027686973624707 ) ) ;
#34143=EDGE_LOOP ( 'NONE', ( #9971, #2125, #11689, #34445 ) ) ;
#34286=CARTESIAN_POINT ( 'NONE',  ( 0.000000000000000000, 0.000000000000000000, -4.974599999999998801 ) ) ;
#34292=CARTESIAN_POINT ( 'NONE',  ( -1.243802165048909503, 3.900692638707381921, -3.223146290109805800 ) ) ;
#34311=B_SPLINE_CURVE_WITH_KNOTS ( 'NONE', 3,
 ( #37704, #32039, #2123, #7823, #17914, #31189 ),
 .UNSPECIFIED., .F., .F.,
 ( 4, 2, 4 ),
 ( 0.003358874760055551890, 0.004541967308452098118, 0.005725059856848645212 ),
 .UNSPECIFIED. ) ;
#34355=CARTESIAN_POINT ( 'NONE',  ( 4.211405965630455661, 2.460463115436283932, -3.751298928144577882 ) ) ;
#34356=ORIENTED_EDGE ( 'NONE', *, *, #27048, .F. ) ;
#34392=CARTESIAN_POINT ( 'NONE',  ( -4.024497503033519941, 2.323544716729375459, -3.572167766733379768 ) ) ;
#34394=EDGE_LOOP ( 'NONE', ( #35574, #16430 ) ) ;
#34398=CARTESIAN_POINT ( 'NONE',  ( 2.548804901056335857E-15, 4.736522675502163437, -3.681124513963624612 ) ) ;
#34406=EDGE_CURVE ( 'NONE', #31862, #9725, #2015, .T. ) ;
#34445=ORIENTED_EDGE ( 'NONE', *, *, #15309, .F. ) ;
#34455=CARTESIAN_POINT ( 'NONE',  ( 0.000000000000000000, 0.000000000000000000, -4.974599999999998801 ) ) ;
#34469=ORIENTED_EDGE ( 'NONE', *, *, #4895, .F. ) ;
#34482=EDGE_CURVE ( 'NONE', #28956, #39558, #30760, .T. ) ;
#34518=ORIENTED_EDGE ( 'NONE', *, *, #42887, .T. ) ;
#34525=CARTESIAN_POINT ( 'NONE',  ( -5.560781378645575757, 6.809993116116508640E-16, -4.000000000000000000 ) ) ;
#34580=ORIENTED_EDGE ( 'NONE', *, *, #1184, .T. ) ;
#34588=VECTOR ( 'NONE', #11672, 1000.000000000000000 ) ;
#34623=CARTESIAN_POINT ( 'NONE',  ( 1.734723475976807094E-15, 4.618802153517012954, -0.4999999999999995559 ) ) ;
#34637=CARTESIAN_POINT ( 'NONE',  ( -2.171643655288372443, 3.365003104552320767, 2.541098841762897165E-18 ) ) ;
#34642=( BOUNDED_SURFACE ( )  B_SPLINE_SURFACE ( 3, 2, ( 
 ( #8479, #5204, #18567 ),
 ( #39847, #36579, #6272 ),
 ( #29869, #26150, #26784 ),
 ( #19834, #12629, #29213 ),
 ( #23320, #6478, #23118 ),
 ( #42911, #32465, #9973 ) ),
 .UNSPECIFIED., .F., .F., .F. ) 
 B_SPLINE_SURFACE_WITH_KNOTS ( ( 4, 2, 4 ),
 ( 3, 3 ),
 ( 0.02032853247518126918, 0.02278863295364821906, 0.02524873343211516893 ),
 ( 0.000000000000000000, 1.000000000000000000 ),
 .UNSPECIFIED. ) 
 GEOMETRIC_REPRESENTATION_ITEM ( )  RATIONAL_B_SPLINE_SURFACE ( (
 ( 1.000000000000000000, 0.8047781615896838492, 1.000000000000000000),
 ( 1.000000000000000000, 0.8123767586288186404, 1.000000000000000000),
 ( 1.000000000000000000, 0.8190662415565814758, 1.000000000000000000),
 ( 1.000000000000000000, 0.8192361015667604107, 1.000000000000000000),
 ( 1.000000000000000000, 0.8126135807104967190, 1.000000000000000000),
 ( 1.000000000000000000, 0.8047712338318580017, 1.000000000000000000) ) ) 
 REPRESENTATION_ITEM ( '' )  SURFACE ( )  );
#34646=CARTESIAN_POINT ( 'NONE',  ( 0.6640947660595348800, -4.471078309994175548, -3.602146406945708090 ) ) ;
#34683=CARTESIAN_POINT ( 'NONE',  ( -4.000000000000000000, 0.000000000000000000, 0.000000000000000000 ) ) ;
#34735=CARTESIAN_POINT ( 'NONE',  ( -4.236525694536558362, 2.416953475386465211, -3.751298745799836354 ) ) ;
#34801=CARTESIAN_POINT ( 'NONE',  ( -4.000000000000000000, 1.941961291383472732, -0.3515519931180205448 ) ) ;
#34814=EDGE_LOOP ( 'NONE', ( #9621, #23288, #24224, #11226, #39338 ) ) ;
#34861=CARTESIAN_POINT ( 'NONE',  ( -0.02448733951239248641, -4.877042772274742255, -3.751161874094027571 ) ) ;
#34951=ORIENTED_EDGE ( 'NONE', *, *, #7947, .T. ) ;
#34961=CARTESIAN_POINT ( 'NONE',  ( -4.204015924366189871, 1.626724848190922446, -3.610627190413390419 ) ) ;
#35151=CARTESIAN_POINT ( 'NONE',  ( -0.5276280594146446346, 4.314175951381965746, -3.320322319201721495 ) ) ;
#35337=VERTEX_POINT ( 'NONE', #11245 ) ;
#35350=CARTESIAN_POINT ( 'NONE',  ( -4.000000000000000000, -2.309401076758515803, -0.4999999999999995559 ) ) ;
#35372=CARTESIAN_POINT ( 'NONE',  ( 4.000000000000000000, 0.000000000000000000, 0.000000000000000000 ) ) ;
#35441=FACE_OUTER_BOUND ( 'NONE', #5376, .T. ) ;
#35503=CARTESIAN_POINT ( 'NONE',  ( 1.567478505476134606E-15, 4.618802153517012066, -3.433295621305382905 ) ) ;
#35574=ORIENTED_EDGE ( 'NONE', *, *, #22902, .F. ) ;
#35584=CARTESIAN_POINT ( 'NONE',  ( -4.000000000000000000, -1.680117682357936904, -3.316611593218794951 ) ) ;
#35715=ORIENTED_EDGE ( 'NONE', *, *, #8211, .T. ) ;
#35762=CYLINDRICAL_SURFACE ( 'NONE', #11914, 2.100000000000000089 ) ;
#35824=ORIENTED_EDGE ( 'NONE', *, *, #39889, .T. ) ;
#35866=ORIENTED_EDGE ( 'NONE', *, *, #13712, .T. ) ;
#35871=CARTESIAN_POINT ( 'NONE',  ( 0.000000000000000000, 0.000000000000000000, -4.000000000000000000 ) ) ;
#35894=CARTESIAN_POINT ( 'NONE',  ( -6.259644161404860030E-16, -4.618802153517027165, -3.433295621305388234 ) ) ;
#35906=CARTESIAN_POINT ( 'NONE',  ( -1.747541505913277282, 3.837784562140256650, -3.503702292528906526 ) ) ;
#35926=ADVANCED_BREP_SHAPE_REPRESENTATION ( '', ( #28157, #13552 ), #41354 ) ;
#36056=VECTOR ( 'NONE', #3802, 999.9999999999998863 ) ;
#36117=DIRECTION ( 'NONE',  ( -0.000000000000000000, -0.000000000000000000, 1.000000000000000000 ) ) ;
#36120=CARTESIAN_POINT ( 'NONE',  ( -3.264650091097280831E-13, -4.796980096169642493, -3.721999068284424617 ) ) ;
#36139=CARTESIAN_POINT ( 'NONE',  ( -4.211140560182196957, -2.431303136016552013, -3.745885042887436178 ) ) ;
#36221=EDGE_CURVE ( 'NONE', #26591, #14112, #22362, .T. ) ;
#36241=DIRECTION ( 'NONE',  ( -1.000000000000000000, 0.000000000000000000, 0.000000000000000000 ) ) ;
#36280=AXIS2_PLACEMENT_3D ( 'NONE', #27442, #30719, #4069 ) ;
#36281=( BOUNDED_SURFACE ( )  B_SPLINE_SURFACE ( 3, 2, ( 
 ( #10996, #1357, #38004 ),
 ( #21497, #4856, #37366 ),
 ( #20844, #1572, #28223 ),
 ( #15147, #28448, #14263 ),
 ( #35584, #5704, #22546 ),
 ( #19483, #18653, #8552 ) ),
 .UNSPECIFIED., .F., .F., .F. ) 
 B_SPLINE_SURFACE_WITH_KNOTS ( ( 4, 2, 4 ),
 ( 3, 3 ),
 ( 0.02027752710269158445, 0.02273781595091097299, 0.02519810479913036153 ),
 ( 0.000000000000000000, 1.000000000000000000 ),
 .UNSPECIFIED. ) 
 GEOMETRIC_REPRESENTATION_ITEM ( )  RATIONAL_B_SPLINE_SURFACE ( (
 ( 1.000000000000000000, 0.8047781431712808242, 1.000000000000000000),
 ( 1.000000000000000000, 0.8123773247083928561, 1.000000000000000000),
 ( 1.000000000000000000, 0.8190670192154906326, 1.000000000000000000),
 ( 1.000000000000000000, 0.8192353552912178261, 1.000000000000000000),
 ( 1.000000000000000000, 0.8126132098226825917, 1.000000000000000000),
 ( 1.000000000000000000, 0.8047712465856394770, 1.000000000000000000) ) ) 
 REPRESENTATION_ITEM ( '' )  SURFACE ( )  );
#36323=CARTESIAN_POINT ( 'NONE',  ( 0.000000000000000000, 0.000000000000000000, -0.3080913168122742518 ) ) ;
#36369=AXIS2_PLACEMENT_3D ( 'NONE', #34455, #1069, #10478 ) ;
#36370=CARTESIAN_POINT ( 'NONE',  ( 4.101954839143060028, 2.368264730582927857, -3.681130640444267854 ) ) ;
#36419=CARTESIAN_POINT ( 'NONE',  ( 4.000000000000000000, 0.3987449864460005378, -0.01220643443059817035 ) ) ;
#36425=CARTESIAN_POINT ( 'NONE',  ( -4.000000000000000000, -2.309401076758512694, -5.000000000000000000 ) ) ;
#36454=ORIENTED_EDGE ( 'NONE', *, *, #23962, .T. ) ;
#36487=DIRECTION ( 'NONE',  ( 0.000000000000000000, 0.000000000000000000, 1.000000000000000000 ) ) ;
#36508=FACE_OUTER_BOUND ( 'NONE', #3653, .T. ) ;
#36532=FACE_OUTER_BOUND ( 'NONE', #59, .T. ) ;
#36551=CARTESIAN_POINT ( 'NONE',  ( 0.000000000000000000, 0.000000000000000000, -4.000000000000000000 ) ) ;
#36567=ADVANCED_FACE ( 'NONE', ( #960 ), #36852, .T. ) ;
#36579=CARTESIAN_POINT ( 'NONE',  ( -3.453038570459499024, -2.625189405340453419, -3.535263753545272891 ) ) ;
#36668=( LENGTH_UNIT ( ) NAMED_UNIT ( * ) SI_UNIT ( .MILLI., .METRE. ) );
#36735=CARTESIAN_POINT ( 'NONE',  ( 0.6810597143197052450, 4.461075778259290914, -3.598441714920602053 ) ) ;
#36809=CARTESIAN_POINT ( 'NONE',  ( -4.154094228333456762, 2.398367420968013253, -3.721909803043220055 ) ) ;
#36852=CONICAL_SURFACE ( 'NONE', #24351, 4.000000000000000000, 0.8911886515913786111 ) ;
#36958=CARTESIAN_POINT ( 'NONE',  ( 1.411581201560190495E-15, 4.862606272033091592, -3.745885042887436622 ) ) ;
#36977=CARTESIAN_POINT ( 'NONE',  ( 4.000000000000000000, -1.677850389431204459, -3.535268758346977513 ) ) ;
#36997=CIRCLE ( 'NONE', #14742, 5.560781378645573980 ) ;
#37010=ORIENTED_EDGE ( 'NONE', *, *, #13241, .T. ) ;
#37163=CARTESIAN_POINT ( 'NONE',  ( 1.390230914382191596, 4.043987460488659202, -3.502507215260488582 ) ) ;
#37175=( BOUNDED_SURFACE ( )  B_SPLINE_SURFACE ( 3, 2, ( 
 ( #9514, #22867, #39598 ),
 ( #4019, #36977, #744 ),
 ( #37407, #20890, #297 ),
 ( #27395, #40661, #14104 ),
 ( #21102, #7087, #10377 ),
 ( #27620, #23713, #34355 ) ),
 .UNSPECIFIED., .F., .F., .F. ) 
 B_SPLINE_SURFACE_WITH_KNOTS ( ( 4, 2, 4 ),
 ( 3, 3 ),
 ( 0.02027065861071770947, 0.02273072267836921331, 0.02519078674602071716 ),
 ( 0.000000000000000000, 1.000000000000000000 ),
 .UNSPECIFIED. ) 
 GEOMETRIC_REPRESENTATION_ITEM ( )  RATIONAL_B_SPLINE_SURFACE ( (
 ( 1.000000000000000000, 0.8047781708337304885, 1.000000000000000000),
 ( 1.000000000000000000, 0.8123765190705307671, 1.000000000000000000),
 ( 1.000000000000000000, 0.8190656277163975707, 1.000000000000000000),
 ( 1.000000000000000000, 0.8192366903512159348, 1.000000000000000000),
 ( 1.000000000000000000, 0.8126138454302893610, 1.000000000000000000),
 ( 1.000000000000000000, 0.8047712246031417660, 1.000000000000000000) ) ) 
 REPRESENTATION_ITEM ( '' )  SURFACE ( )  );
#37190=DIRECTION ( 'NONE',  ( -1.000000000000000000, 0.000000000000000000, 0.000000000000000000 ) ) ;
#37197=DIRECTION ( 'NONE',  ( 1.000000000000000000, 0.000000000000000000, 0.000000000000000000 ) ) ;
#37244=CARTESIAN_POINT ( 'NONE',  ( -0.3208286057739654917, 4.433571671609680465, -0.3503314178412548774 ) ) ;
#37295=CARTESIAN_POINT ( 'NONE',  ( 4.000000000000000888, 1.563622288139206118, -0.2253451193528334950 ) ) ;
#37358=AXIS2_PLACEMENT_3D ( 'NONE', #35871, #41996, #6002 ) ;
#37366=CARTESIAN_POINT ( 'NONE',  ( -4.204114297095464359, 1.660363174096617156, -3.602136431857887011 ) ) ;
#37407=CARTESIAN_POINT ( 'NONE',  ( 4.000000000000000000, -0.8732470631449981147, -3.223155494240760088 ) ) ;
#37437=SHAPE_REPRESENTATION ( 'hex flange nut gradea_iso_ISO - 4161 - M5 - N', ( #13552 ), #41354 ) ;
#37442=VERTEX_POINT ( 'NONE', #10270 ) ;
#37647=AXIS2_PLACEMENT_3D ( 'NONE', #36551, #6676, #33306 ) ;
#37694=CARTESIAN_POINT ( 'NONE',  ( 1.360585162435110629, -4.061296242128317857, -3.505054077164905024 ) ) ;
#37704=CARTESIAN_POINT ( 'NONE',  ( 4.000000000000000000, -2.309401076758516691, -0.4999999999999995559 ) ) ;
#37738=B_SPLINE_CURVE_WITH_KNOTS ( 'NONE', 3,
 ( #20379, #33225, #20830, #33644, #26687, #30392, #39953, #3518 ),
 .UNSPECIFIED., .F., .F.,
 ( 4, 2, 2, 4 ),
 ( 2.465131517075058656E-07, 0.001183067374689851080, 0.001774477805458923299, 0.002365888236227995517 ),
 .UNSPECIFIED. ) ;
#37775=CARTESIAN_POINT ( 'NONE',  ( -4.175648173966055587, 2.207990556236529844, -3.469390959564062626 ) ) ;
#37796=CARTESIAN_POINT ( 'NONE',  ( -4.211140560182196957, 2.431303136016537803, -3.745885042887433514 ) ) ;
#37820=B_SPLINE_CURVE_WITH_KNOTS ( 'NONE', 3,
 ( #20491, #3197, #29877, #33758, #23550, #10427, #13936, #7356 ),
 .UNSPECIFIED., .F., .F.,
 ( 4, 2, 2, 4 ),
 ( 2.465131517071610173E-07, 0.001183067374689837636, 0.001774477805458902699, 0.002365888236227967761 ),
 .UNSPECIFIED. ) ;
#37906=CARTESIAN_POINT ( 'NONE',  ( 4.175648173966055587, -2.207990556236547608, -3.469390959564065291 ) ) ;
#37933=ORIENTED_EDGE ( 'NONE', *, *, #15871, .F. ) ;
#37942=CARTESIAN_POINT ( 'NONE',  ( -4.000000000000000000, -1.942223658245633811, -0.3516579909967644246 ) ) ;
#38004=CARTESIAN_POINT ( 'NONE',  ( -4.211399284164270895, 2.459729995988205964, -3.751162237960538715 ) ) ;
#38009=TOROIDAL_SURFACE ( 'NONE', #40766, 5.384454397937118664, 0.5155456020628804703 ) ;
#38112=DIRECTION ( 'NONE',  ( 1.000000000000000000, 0.000000000000000000, 0.000000000000000000 ) ) ;
#38129=DIRECTION ( 'NONE',  ( 1.000000000000000000, 0.000000000000000000, 0.000000000000000000 ) ) ;
#38149=CIRCLE ( 'NONE', #38855, 2.499999999999999556 ) ;
#38163=ORIENTED_EDGE ( 'NONE', *, *, #41388, .T. ) ;
#38215=CARTESIAN_POINT ( 'NONE',  ( -3.455068668934486276, 2.624017327439035707, -3.316620875263955437 ) ) ;
#38343=CARTESIAN_POINT ( 'NONE',  ( 3.455068668934414777, -2.624017327439094327, -3.316620875263732504 ) ) ;
#38370=ORIENTED_EDGE ( 'NONE', *, *, #34054, .F. ) ;
#38420=CARTESIAN_POINT ( 'NONE',  ( -4.141042297810615835, 2.227970268150415656, -3.687027686973619822 ) ) ;
#38435=DIRECTION ( 'NONE',  ( -0.000000000000000000, -0.000000000000000000, 1.000000000000000000 ) ) ;
#38486=CARTESIAN_POINT ( 'NONE',  ( 0.000000000000000000, 0.000000000000000000, -5.000000000000000000 ) ) ;
#38528=CARTESIAN_POINT ( 'NONE',  ( 0.000000000000000000, 0.000000000000000000, -5.000000000000000000 ) ) ;
#38719=LINE ( 'NONE', #28522, #24692 ) ;
#38758=CARTESIAN_POINT ( 'NONE',  ( -2.855764796983342624, 2.970025579236414082, -0.09382832055445475272 ) ) ;
#38855=AXIS2_PLACEMENT_3D ( 'NONE', #43027, #9671, #39741 ) ;
#38985=VERTEX_POINT ( 'NONE', #15261 ) ;
#39002=CARTESIAN_POINT ( 'NONE',  ( 4.000000000000000000, 2.309401076758497151, -3.433295621305379353 ) ) ;
#39101=CARTESIAN_POINT ( 'NONE',  ( -2.000000000000007550, -3.464101615137749945, 0.000000000000000000 ) ) ;
#39172=CIRCLE ( 'NONE', #28070, 2.100000000000000089 ) ;
#39176=CARTESIAN_POINT ( 'NONE',  ( 4.000000000000000000, -2.309401076758514915, -5.000000000000000000 ) ) ;
#39210=ORIENTED_EDGE ( 'NONE', *, *, #34482, .F. ) ;
#39296=AXIS2_PLACEMENT_3D ( 'NONE', #22499, #23346, #26603 ) ;
#39338=ORIENTED_EDGE ( 'NONE', *, *, #12619, .T. ) ;
#39391=VECTOR ( 'NONE', #17363, 1000.000000000000000 ) ;
#39405=( GEOMETRIC_REPRESENTATION_CONTEXT ( 3 ) GLOBAL_UNCERTAINTY_ASSIGNED_CONTEXT ( ( #754 ) ) GLOBAL_UNIT_ASSIGNED_CONTEXT ( ( #18890, #10246, #32147 ) ) REPRESENTATION_CONTEXT ( 'NONE', 'WORKASPACE' ) );
#39418=EDGE_CURVE ( 'NONE', #40010, #24356, #36997, .T. ) ;
#39437=AXIS2_PLACEMENT_3D ( 'NONE', #42132, #42357, #12505 ) ;
#39487=EDGE_LOOP ( 'NONE', ( #84, #6191, #21822, #21129 ) ) ;
#39507=EDGE_CURVE ( 'NONE', #880, #1858, #27976, .T. ) ;
#39558=VERTEX_POINT ( 'NONE', #15415 ) ;
#39576=EDGE_CURVE ( 'NONE', #14112, #15592, #3265, .T. ) ;
#39598=CARTESIAN_POINT ( 'NONE',  ( 4.211399257449709665, -2.459727064652517114, -3.751161691472417736 ) ) ;
#39622=CARTESIAN_POINT ( 'NONE',  ( -4.101948962585905356, -2.368261337751088824, -3.681124513963624167 ) ) ;
#39665=CARTESIAN_POINT ( 'NONE',  ( 4.000000000000000000, -2.309401076758514915, -3.433295621305383349 ) ) ;
#39676=CARTESIAN_POINT ( 'NONE',  ( 4.154306624731035846, -2.398490048085128556, -3.721999068284417955 ) ) ;
#39687=DIRECTION ( 'NONE',  ( -1.000000000000000000, 0.000000000000000000, 0.000000000000000000 ) ) ;
#39708=ADVANCED_FACE ( 'NONE', ( #35441 ), #2681, .T. ) ;
#39741=DIRECTION ( 'NONE',  ( 1.000000000000000000, 0.000000000000000000, 0.000000000000000000 ) ) ;
#39826=EDGE_LOOP ( 'NONE', ( #2248, #22281, #15452, #30167, #22739, #13585, #195 ) ) ;
#39847=CARTESIAN_POINT ( 'NONE',  ( -3.472371940586054251, -2.614027278893156669, -3.320322319202162031 ) ) ;
#39885=CARTESIAN_POINT ( 'NONE',  ( 4.024499207728657879, -2.323545700935587988, -3.572172305156509964 ) ) ;
#39889=EDGE_CURVE ( 'NONE', #1858, #40010, #40506, .T. ) ;
#39936=EDGE_CURVE ( 'NONE', #6132, #11201, #41215, .T. ) ;
#39953=CARTESIAN_POINT ( 'NONE',  ( 1.828356344711641102, 3.563200125723180900, -5.433716356636336675E-16 ) ) ;
#39978=LINE ( 'NONE', #3982, #39391 ) ;
#39988=CARTESIAN_POINT ( 'NONE',  ( 2.742827927723449299, 3.035229711104609596, -3.433252694550591233 ) ) ;
#39998=EDGE_CURVE ( 'NONE', #6210, #19145, #32879, .T. ) ;
#40010=VERTEX_POINT ( 'NONE', #34525 ) ;
#40070=DIRECTION ( 'NONE',  ( -0.000000000000000000, -0.000000000000000000, 1.000000000000000000 ) ) ;
#40087=CARTESIAN_POINT ( 'NONE',  ( 4.000000000000000000, 2.309401076758497151, -3.433295621305379353 ) ) ;
#40118=CARTESIAN_POINT ( 'NONE',  ( -6.473970235329672780E-16, -4.862606272033106691, -3.745885042887442395 ) ) ;
#40178=ORIENTED_EDGE ( 'NONE', *, *, #6370, .T. ) ;
#40184=CONICAL_SURFACE ( 'NONE', #4668, 5.560781378645573980, 1.221730476396046816 ) ;
#40191=CIRCLE ( 'NONE', #3275, 4.000000000000000000 ) ;
#40218=CARTESIAN_POINT ( 'NONE',  ( 4.175002511812151873, 2.208363329454889445, -3.469254087858244073 ) ) ;
#40287=CARTESIAN_POINT ( 'NONE',  ( -4.000000000000000000, 2.309401076758498483, -3.433295621305379353 ) ) ;
#40319=EDGE_CURVE ( 'NONE', #959, #35337, #92, .T. ) ;
#40323=CARTESIAN_POINT ( 'NONE',  ( -3.999999999999999112, 1.539600717838996324, -3.300726591567078039 ) ) ;
#40430=EDGE_LOOP ( 'NONE', ( #1535, #15929 ) ) ;
#40446=DIRECTION ( 'NONE',  ( -0.000000000000000000, -0.000000000000000000, 1.000000000000000000 ) ) ;
#40506=CIRCLE ( 'NONE', #7066, 0.5155456020628804703 ) ;
#40549=CARTESIAN_POINT ( 'NONE',  ( -4.211140560182196957, -2.431303136016552013, -3.745885042887436178 ) ) ;
#40585=CARTESIAN_POINT ( 'NONE',  ( 0.000000000000000000, 0.000000000000000000, -4.000000000000000000 ) ) ;
#40619=EDGE_LOOP ( 'NONE', ( #19472, #24510, #19052, #518, #41313 ) ) ;
#40644=CARTESIAN_POINT ( 'NONE',  ( 0.000000000000000000, 0.000000000000000000, -25.03750572909317285 ) ) ;
#40645=AXIS2_PLACEMENT_3D ( 'NONE', #9802, #22723, #26186 ) ;
#40647=B_SPLINE_CURVE_WITH_KNOTS ( 'NONE', 3,
 ( #29196, #2739, #32232, #28978, #19179, #6042, #40682, #7546 ),
 .UNSPECIFIED., .F., .F.,
 ( 4, 2, 2, 4 ),
 ( 2.465131517390770070E-07, 0.001183067374689869946, 0.001774477805458935659, 0.002365888236228001588 ),
 .UNSPECIFIED. ) ;
#40661=CARTESIAN_POINT ( 'NONE',  ( 4.000000000000000888, 0.8228435280416209752, -3.430609588141487976 ) ) ;
#40682=CARTESIAN_POINT ( 'NONE',  ( -1.828356344711647319, -3.563200125723192002, -1.076197711133951296E-14 ) ) ;
#40766=AXIS2_PLACEMENT_3D ( 'NONE', #31892, #27779, #21247 ) ;
#40910=APPLICATION_CONTEXT ( 'automotive_design' ) ;
#40982=DIRECTION ( 'NONE',  ( -0.000000000000000000, -0.000000000000000000, 1.000000000000000000 ) ) ;
#40991=CARTESIAN_POINT ( 'NONE',  ( 2.000000000000005329, -3.464101615137751722, 0.000000000000000000 ) ) ;
#41010=DIRECTION ( 'NONE',  ( -1.000000000000000000, 0.000000000000000000, 0.000000000000000000 ) ) ;
#41041=CARTESIAN_POINT ( 'NONE',  ( -2.807080416178626692, 3.225969019225154444, -3.502507215260441065 ) ) ;
#41052=ADVANCED_FACE ( 'NONE', ( #13202 ), #73, .T. ) ;
#41079=CARTESIAN_POINT ( 'NONE',  ( 2.449848172108560096, 3.432307619358740514, -3.503702292528905637 ) ) ;
#41088=DIRECTION ( 'NONE',  ( -1.000000000000000000, 0.000000000000000000, 0.000000000000000000 ) ) ;
#41162=CARTESIAN_POINT ( 'NONE',  ( -2.345747346278108214, 3.264484291692489215, -0.01223254789873409049 ) ) ;
#41193=FACE_OUTER_BOUND ( 'NONE', #39487, .T. ) ;
#41215=B_SPLINE_CURVE_WITH_KNOTS ( 'NONE', 3,
 ( #11863, #5070, #31920, #11644, #18661, #4406 ),
 .UNSPECIFIED., .F., .F.,
 ( 4, 2, 4 ),
 ( 0.002452478801916361129, 0.003676905084148001344, 0.004901331366379641126 ),
 .UNSPECIFIED. ) ;
#41305=CARTESIAN_POINT ( 'NONE',  ( 0.000000000000000000, 0.000000000000000000, -0.2800830152838844622 ) ) ;
#41313=ORIENTED_EDGE ( 'NONE', *, *, #16943, .F. ) ;
#41325=ORIENTED_EDGE ( 'NONE', *, *, #17492, .T. ) ;
#41354=( GEOMETRIC_REPRESENTATION_CONTEXT ( 3 ) GLOBAL_UNCERTAINTY_ASSIGNED_CONTEXT ( ( #26984 ) ) GLOBAL_UNIT_ASSIGNED_CONTEXT ( ( #211, #29726, #19497 ) ) REPRESENTATION_CONTEXT ( 'NONE', 'WORKASPACE' ) );
#41387=CARTESIAN_POINT ( 'NONE',  ( 2.712762565639649015, -3.052587955997662306, -3.430618716626630871 ) ) ;
#41388=EDGE_CURVE ( 'NONE', #7662, #35337, #7918, .T. ) ;
#41483=CARTESIAN_POINT ( 'NONE',  ( 3.511755186886750923, -2.826662030176382956, -3.597382984111582083 ) ) ;
#41598=CARTESIAN_POINT ( 'NONE',  ( -2.500000000000000444, 3.061616997868383634E-16, -5.000000000000000888 ) ) ;
#41929=DIRECTION ( 'NONE',  ( -0.8191520442889902442, 0.000000000000000000, -0.5735764363510482688 ) ) ;
#41996=DIRECTION ( 'NONE',  ( 0.000000000000000000, 0.000000000000000000, -1.000000000000000000 ) ) ;
#42025=CARTESIAN_POINT ( 'NONE',  ( -4.000000000000000000, 2.309401076758498483, -0.4999999999999927280 ) ) ;
#42132=CARTESIAN_POINT ( 'NONE',  ( 0.000000000000000000, 0.000000000000000000, -0.2800830152838844622 ) ) ;
#42246=CARTESIAN_POINT ( 'NONE',  ( -0.6937372685066653943, 4.453844082567723461, -3.610536846335889116 ) ) ;
#42249=DIRECTION ( 'NONE',  ( -1.000000000000000000, 0.000000000000000000, 0.000000000000000000 ) ) ;
#42300=ORIENTED_EDGE ( 'NONE', *, *, #5774, .T. ) ;
#42313=CARTESIAN_POINT ( 'NONE',  ( 1.734723475976807094E-15, 4.618802153517012954, -0.4999999999999995559 ) ) ;
#42327=FACE_OUTER_BOUND ( 'NONE', #34143, .T. ) ;
#42336=ORIENTED_EDGE ( 'NONE', *, *, #1044, .T. ) ;
#42357=DIRECTION ( 'NONE',  ( 0.000000000000000000, 0.000000000000000000, -1.000000000000000000 ) ) ;
#42423=EDGE_CURVE ( 'NONE', #29146, #33962, #5800, .T. ) ;
#42437=CARTESIAN_POINT ( 'NONE',  ( 4.000000000000000000, 2.309401076758497151, -3.433295621305379353 ) ) ;
#42470=CARTESIAN_POINT ( 'NONE',  ( -3.333333333333335258, 2.694301256218251783, -3.300726591567079815 ) ) ;
#42498=ORIENTED_EDGE ( 'NONE', *, *, #34054, .T. ) ;
#42509=FACE_OUTER_BOUND ( 'NONE', #22017, .T. ) ;
#42544=DIRECTION ( 'NONE',  ( 0.000000000000000000, 0.000000000000000000, 1.000000000000000000 ) ) ;
#42545=EDGE_LOOP ( 'NONE', ( #2299, #24489 ) ) ;
#42598=ORIENTED_EDGE ( 'NONE', *, *, #26699, .T. ) ;
#42614=CARTESIAN_POINT ( 'NONE',  ( 0.000000000000000000, 0.000000000000000000, 0.000000000000000000 ) ) ;
#42622=LINE ( 'NONE', #12773, #19777 ) ;
#42654=CARTESIAN_POINT ( 'NONE',  ( 2.100000000000000089, 0.000000000000000000, -0.2800830152838844622 ) ) ;
#42696=CARTESIAN_POINT ( 'NONE',  ( 4.197393957002303999, 7.772902908466098641E-14, -3.503767560748929810 ) ) ;
#42790=EDGE_CURVE ( 'NONE', #6132, #24356, #38719, .T. ) ;
#42887=EDGE_CURVE ( 'NONE', #24669, #959, #15429, .T. ) ;
#42911=CARTESIAN_POINT ( 'NONE',  ( 0.1756481739660539498, -4.720212674038995360, -3.469390959564070620 ) ) ;
#42915=DIRECTION ( 'NONE',  ( 0.000000000000000000, 0.000000000000000000, 1.000000000000000000 ) ) ;
#42999=SURFACE_SIDE_STYLE ('',( #33413 ) ) ;
#43027=CARTESIAN_POINT ( 'NONE',  ( 0.000000000000000000, 0.000000000000000000, 3.469446951953614189E-15 ) ) ;
#43029=EDGE_LOOP ( 'NONE', ( #2936, #16640, #12145 ) ) ;
#43157=CARTESIAN_POINT ( 'NONE',  ( 3.999999999999999112, -1.539600717839012978, -3.300726591567080703 ) ) ;
#43162=CARTESIAN_POINT ( 'NONE',  ( 2.000000000000005329, -3.464101615137751722, 0.000000000000000000 ) ) ;
#43175=SURFACE_STYLE_FILL_AREA ( #29914 ) ;
#43179=DIRECTION ( 'NONE',  ( 1.000000000000000000, 0.000000000000000000, 0.000000000000000000 ) ) ;
ENDSEC;
END-ISO-10303-21;
